ISO-10303-21;
HEADER;
FILE_DESCRIPTION (('STEP AP214'),
    '1' );
FILE_NAME ('hexagon nut style 1_is_IS 1364-3 - M12-W-N.step',
    '2026-10-26T19:46:16',
    ( '' ),
    ( '' ),
    'SwSTEP 2.0',
    'SolidWorks 2025',
    '' );
FILE_SCHEMA (( 'AUTOMOTIVE_DESIGN' ));
ENDSEC;

DATA;
#231=CARTESIAN_POINT ( 'NONE',  ( -9.000000000000000000, 0.000000000000000000, -10.20000000000000462 ) ) ;
#327=VERTEX_POINT ( 'NONE', #22463 ) ;
#668=EDGE_CURVE ( 'NONE', #30116, #59754, #15135, .T. ) ;
#686=ORIENTED_EDGE ( 'NONE', *, *, #62121, .F. ) ;
#711=CONICAL_SURFACE ( 'NONE', #72949, 8.999999999999998224, 1.047197551196595855 ) ;
#866=B_SPLINE_CURVE_WITH_KNOTS ( 'NONE', 3,
 ( #46307, #1054, #11983, #45563, #68576, #58029 ),
 .UNSPECIFIED., .F., .F.,
 ( 4, 2, 4 ),
 ( 0.009270618776430220032, 0.01189894710419331543, 0.01452727543195641083 ),
 .UNSPECIFIED. ) ;
#904=LINE ( 'NONE', #74455, #27987 ) ;
#1042=AXIS2_PLACEMENT_3D ( 'NONE', #73505, #72388, #67110 ) ;
#1054=CARTESIAN_POINT ( 'NONE',  ( 9.000000000000001776, -4.351040328464082840, -0.5598847297401613465 ) ) ;
#1265=DIRECTION ( 'NONE',  ( -1.000000000000000000, 0.000000000000000000, 0.000000000000000000 ) ) ;
#1284=DIRECTION ( 'NONE',  ( 1.000000000000000000, 0.000000000000000000, 0.000000000000000000 ) ) ;
#1515=ADVANCED_FACE ( 'NONE', ( #56942 ), #56198, .F. ) ;
#1518=( LENGTH_UNIT ( ) NAMED_UNIT ( * ) SI_UNIT ( .MILLI., .METRE. ) );
#1869=VECTOR ( 'NONE', #26738, 1000.000000000000000 ) ;
#1919=ORIENTED_EDGE ( 'NONE', *, *, #66888, .F. ) ;
#1957=ORIENTED_EDGE ( 'NONE', *, *, #36684, .F. ) ;
#2044=CARTESIAN_POINT ( 'NONE',  ( 6.023803224821318913, -6.914460432017358826, -0.07661102881318833380 ) ) ;
#2080=EDGE_CURVE ( 'NONE', #41819, #4091, #11163, .T. ) ;
#2154=EDGE_CURVE ( 'NONE', #39667, #41903, #29258, .T. ) ;
#2233=ORIENTED_EDGE ( 'NONE', *, *, #30702, .F. ) ;
#2393=EDGE_CURVE ( 'NONE', #41819, #50322, #11449, .T. ) ;
#2441=CARTESIAN_POINT ( 'NONE',  ( -9.000000000000000000, 5.196152422706624918, -10.80000000000000071 ) ) ;
#2470=AXIS2_PLACEMENT_3D ( 'NONE', #61580, #32929, #50250 ) ;
#2743=DIRECTION ( 'NONE',  ( 1.000000000000000000, 0.000000000000000000, 0.000000000000000000 ) ) ;
#2837=ADVANCED_FACE ( 'NONE', ( #2996 ), #60325, .T. ) ;
#2839=DIRECTION ( 'NONE',  ( -1.000000000000000000, 0.000000000000000000, 0.000000000000000000 ) ) ;
#2949=PLANE ( 'NONE',  #6174 ) ;
#2986=DIRECTION ( 'NONE',  ( 0.5000000000000008882, -0.8660254037844381525, 0.000000000000000000 ) ) ;
#2996=FACE_OUTER_BOUND ( 'NONE', #9605, .T. ) ;
#3252=EDGE_CURVE ( 'NONE', #61426, #12586, #43679, .T. ) ;
#3405=ORIENTED_EDGE ( 'NONE', *, *, #68581, .T. ) ;
#3549=ADVANCED_FACE ( 'NONE', ( #55989 ), #60510, .T. ) ;
#3653=CONICAL_SURFACE ( 'NONE', #14450, 5.009999999999998899, 0.9599310885968824758 ) ;
#3700=DIRECTION ( 'NONE',  ( -1.000000000000000000, 0.000000000000000000, 0.000000000000000000 ) ) ;
#3879=CARTESIAN_POINT ( 'NONE',  ( 9.000000000000001776, 0.8785859941773073167, -9.452887691357987840E-16 ) ) ;
#3967=DIRECTION ( 'NONE',  ( 1.000000000000000000, 0.000000000000000000, 0.000000000000000000 ) ) ;
#4091=VERTEX_POINT ( 'NONE', #43092 ) ;
#4182=VECTOR ( 'NONE', #33358, 1000.000000000000000 ) ;
#4329=ORIENTED_EDGE ( 'NONE', *, *, #26977, .F. ) ;
#4425=DIRECTION ( 'NONE',  ( 0.8191520442889924647, 0.000000000000000000, 0.5735764363510451602 ) ) ;
#4491=LINE ( 'NONE', #22953, #26315 ) ;
#4511=CARTESIAN_POINT ( 'NONE',  ( 0.000000000000000000, 0.000000000000000000, -25.03750572909317285 ) ) ;
#4574=DIRECTION ( 'NONE',  ( -0.000000000000000000, -0.000000000000000000, 1.000000000000000000 ) ) ;
#4784=AXIS2_PLACEMENT_3D ( 'NONE', #58687, #41693, #64706 ) ;
#4925=ORIENTED_EDGE ( 'NONE', *, *, #12739, .T. ) ;
#4976=ORIENTED_EDGE ( 'NONE', *, *, #33794, .T. ) ;
#5082=( NAMED_UNIT ( * ) PLANE_ANGLE_UNIT ( ) SI_UNIT ( $, .RADIAN. ) );
#5104=DIRECTION ( 'NONE',  ( 1.000000000000000000, 0.000000000000000000, 0.000000000000000000 ) ) ;
#5128=DIRECTION ( 'NONE',  ( 0.000000000000000000, -0.000000000000000000, 1.000000000000000000 ) ) ;
#5158=CARTESIAN_POINT ( 'NONE',  ( 9.000000000000000000, 5.196152422706622254, -10.80000000000000071 ) ) ;
#5292=DIRECTION ( 'NONE',  ( -1.000000000000000000, 0.000000000000000000, -0.000000000000000000 ) ) ;
#5314=DIRECTION ( 'NONE',  ( 1.000000000000000000, 0.000000000000000000, 0.000000000000000000 ) ) ;
#5376=ORIENTED_EDGE ( 'NONE', *, *, #34898, .F. ) ;
#5431=CARTESIAN_POINT ( 'NONE',  ( 6.938893903907228378E-15, 10.39230484541326938, -10.80000000000000071 ) ) ;
#5444=ORIENTED_EDGE ( 'NONE', *, *, #48808, .F. ) ;
#5461=LINE ( 'NONE', #40157, #20207 ) ;
#5729=ADVANCED_BREP_SHAPE_REPRESENTATION ( '', ( #16403, #57354 ), #14000 ) ;
#5787=EDGE_CURVE ( 'NONE', #65581, #8182, #54295, .T. ) ;
#6174=AXIS2_PLACEMENT_3D ( 'NONE', #67446, #49335, #3700 ) ;
#6180=PLANE ( 'NONE',  #44255 ) ;
#6206=EDGE_CURVE ( 'NONE', #65581, #59754, #34950, .T. ) ;
#6241=ORIENTED_EDGE ( 'NONE', *, *, #38040, .F. ) ;
#6258=CARTESIAN_POINT ( 'NONE',  ( -9.000000000000000000, -5.196152422706644458, -10.20000000000000284 ) ) ;
#6420=CARTESIAN_POINT ( 'NONE',  ( 9.000000000000001776, 0.000000000000000000, -10.80000000000000071 ) ) ;
#6649=ORIENTED_EDGE ( 'NONE', *, *, #13997, .T. ) ;
#6721=VERTEX_POINT ( 'NONE', #62017 ) ;
#6850=CONICAL_SURFACE ( 'NONE', #47762, 5.009999999999998899, 0.9599310885968824758 ) ;
#6930=CARTESIAN_POINT ( 'NONE',  ( -6.401276095387002485, -6.696526368584479805, -0.1469846612282594001 ) ) ;
#7090=EDGE_CURVE ( 'NONE', #56231, #27106, #20614, .T. ) ;
#7148=CARTESIAN_POINT ( 'NONE',  ( 6.401276095386993603, 6.696526368584462041, -0.1469846612282491305 ) ) ;
#7166=UNCERTAINTY_MEASURE_WITH_UNIT (LENGTH_MEASURE( 1.000000000000000082E-05 ), #1518, 'distance_accuracy_value', 'NONE');
#7176=DIRECTION ( 'NONE',  ( -1.000000000000000000, 0.000000000000000000, -0.000000000000000000 ) ) ;
#7194=EDGE_LOOP ( 'NONE', ( #24127, #5444, #62080 ) ) ;
#7200=DIRECTION ( 'NONE',  ( -0.5000000000000012212, -0.8660254037844379305, 0.000000000000000000 ) ) ;
#7208=CONICAL_SURFACE ( 'NONE', #4784, 6.000000000000000000, 0.9599310885968792562 ) ;
#7517=CARTESIAN_POINT ( 'NONE',  ( 6.024380653971844524, 6.914127053141843504, -0.09252763182292059185 ) ) ;
#7599=LINE ( 'NONE', #53257, #31225 ) ;
#7709=ADVANCED_FACE ( 'NONE', ( #25540 ), #48337, .T. ) ;
#7779=ORIENTED_EDGE ( 'NONE', *, *, #24264, .T. ) ;
#7897=ORIENTED_EDGE ( 'NONE', *, *, #10673, .F. ) ;
#7944=CARTESIAN_POINT ( 'NONE',  ( 2.976196775178699294, 8.673996836102547903, -0.07661102881317931323 ) ) ;
#7974=VECTOR ( 'NONE', #12668, 1000.000000000000114 ) ;
#8052=AXIS2_PLACEMENT_3D ( 'NONE', #45662, #28316, #5314 ) ;
#8120=B_SPLINE_CURVE_WITH_KNOTS ( 'NONE', 3,
 ( #12288, #58333, #70013, #47715, #42427, #47354 ),
 .UNSPECIFIED., .F., .F.,
 ( 4, 2, 4 ),
 ( 0.009270618776430214827, 0.01189894710419331370, 0.01452727543195641083 ),
 .UNSPECIFIED. ) ;
#8182=VERTEX_POINT ( 'NONE', #39853 ) ;
#8308=DIRECTION ( 'NONE',  ( -1.000000000000000000, 0.000000000000000000, -0.000000000000000000 ) ) ;
#8398=VERTEX_POINT ( 'NONE', #59440 ) ;
#8404=CARTESIAN_POINT ( 'NONE',  ( 8.999999999999998224, 0.000000000000000000, 0.000000000000000000 ) ) ;
#8490=ORIENTED_EDGE ( 'NONE', *, *, #49092, .F. ) ;
#8497=DIRECTION ( 'NONE',  ( -0.000000000000000000, -0.000000000000000000, 1.000000000000000000 ) ) ;
#8529=ORIENTED_EDGE ( 'NONE', *, *, #33794, .F. ) ;
#8536=EDGE_CURVE ( 'NONE', #47034, #50322, #37915, .T. ) ;
#8609=DIRECTION ( 'NONE',  ( -0.000000000000000000, -0.000000000000000000, 1.000000000000000000 ) ) ;
#8638=EDGE_LOOP ( 'NONE', ( #31683, #59580, #18189, #34371, #30626, #60689 ) ) ;
#8664=FACE_OUTER_BOUND ( 'NONE', #67008, .T. ) ;
#8668=ORIENTED_EDGE ( 'NONE', *, *, #34898, .T. ) ;
#8683=ORIENTED_EDGE ( 'NONE', *, *, #7090, .T. ) ;
#8819=CIRCLE ( 'NONE', #50998, 6.000000000000000000 ) ;
#8881=AXIS2_PLACEMENT_3D ( 'NONE', #65769, #35279, #18278 ) ;
#8892=EDGE_CURVE ( 'NONE', #8398, #13802, #19717, .T. ) ;
#9064=CARTESIAN_POINT ( 'NONE',  ( -4.881900264494508868, -7.573738413550474391, -6.853343576234544043E-15 ) ) ;
#9218=DIRECTION ( 'NONE',  ( 0.000000000000000000, 0.000000000000000000, -1.000000000000000000 ) ) ;
#9336=CARTESIAN_POINT ( 'NONE',  ( -6.000000000000000000, 0.000000000000000000, -10.77459999999999951 ) ) ;
#9394=FACE_OUTER_BOUND ( 'NONE', #47730, .T. ) ;
#9504=DIRECTION ( 'NONE',  ( 0.000000000000000000, 0.000000000000000000, 1.000000000000000000 ) ) ;
#9605=EDGE_LOOP ( 'NONE', ( #13872, #1919, #39821 ) ) ;
#9734=LINE ( 'NONE', #43680, #16613 ) ;
#9747=ORIENTED_EDGE ( 'NONE', *, *, #44016, .T. ) ;
#9833=AXIS2_PLACEMENT_3D ( 'NONE', #5158, #10803, #28150 ) ;
#10052=CARTESIAN_POINT ( 'NONE',  ( -4.500000000000007994, 7.794228634059939154, 0.000000000000000000 ) ) ;
#10122=ORIENTED_EDGE ( 'NONE', *, *, #6206, .T. ) ;
#10333=LINE ( 'NONE', #66925, #4182 ) ;
#10371=CARTESIAN_POINT ( 'NONE',  ( 9.000000000000000000, 5.196152422706622254, -10.20000000000000284 ) ) ;
#10417=CARTESIAN_POINT ( 'NONE',  ( -6.000000000000000000, 0.000000000000000000, -10.77459999999999951 ) ) ;
#10423=CARTESIAN_POINT ( 'NONE',  ( -1.474731560294321397, 9.540868182094907723, -0.3570196857253543077 ) ) ;
#10625=CARTESIAN_POINT ( 'NONE',  ( 5.204170427930421283E-15, 10.39230484541327293, -0.8038475772933779684 ) ) ;
#10673=EDGE_CURVE ( 'NONE', #8182, #39667, #41742, .T. ) ;
#10763=CONICAL_SURFACE ( 'NONE', #27663, 6.000000000000000000, 0.9599310885968792562 ) ;
#10773=DIRECTION ( 'NONE',  ( -1.000000000000000000, 0.000000000000000000, 0.000000000000000000 ) ) ;
#10803=DIRECTION ( 'NONE',  ( -1.000000000000000000, 0.000000000000000000, 0.000000000000000000 ) ) ;
#10860=CONICAL_SURFACE ( 'NONE', #25271, 8.999999999999998224, 1.047197551196595855 ) ;
#10906=CARTESIAN_POINT ( 'NONE',  ( -6.000000000000000000, 7.347880794884119736E-16, 0.000000000000000000 ) ) ;
#10928=CARTESIAN_POINT ( 'NONE',  ( 5.099999999999999645, 0.000000000000000000, -10.80000000000000071 ) ) ;
#10960=ORIENTED_EDGE ( 'NONE', *, *, #11791, .F. ) ;
#11007=CARTESIAN_POINT ( 'NONE',  ( -8.999999999999998224, 0.000000000000000000, 0.000000000000000000 ) ) ;
#11012=EDGE_CURVE ( 'NONE', #63081, #64865, #72775, .T. ) ;
#11163=CIRCLE ( 'NONE', #36472, 8.999999999999998224 ) ;
#11318=CARTESIAN_POINT ( 'NONE',  ( -3.733333029993816776, -8.236864015571837783, -6.823697423080643532E-15 ) ) ;
#11422=DIRECTION ( 'NONE',  ( 0.000000000000000000, 0.000000000000000000, 1.000000000000000000 ) ) ;
#11449=B_SPLINE_CURVE_WITH_KNOTS ( 'NONE', 3,
 ( #66020, #9064, #32076, #18620, #6930, #61112, #32459, #29940 ),
 .UNSPECIFIED., .F., .F.,
 ( 4, 2, 2, 4 ),
 ( 0.005257893453559919252, 0.006567392922673248590, 0.007876892391786578795, 0.01049589133001323574 ),
 .UNSPECIFIED. ) ;
#11791=EDGE_CURVE ( 'NONE', #8182, #65581, #17413, .T. ) ;
#11866=DIRECTION ( 'NONE',  ( -0.000000000000000000, -0.000000000000000000, 1.000000000000000000 ) ) ;
#11983=CARTESIAN_POINT ( 'NONE',  ( 9.000000000000000000, -3.485479754112952300, -0.3552645118408620517 ) ) ;
#12205=CARTESIAN_POINT ( 'NONE',  ( 5.204170427930421283E-15, 10.39230484541327293, -0.8038475772933779684 ) ) ;
#12288=CARTESIAN_POINT ( 'NONE',  ( -9.000000000000000000, -5.196152422706648899, -0.8038475772933779684 ) ) ;
#12305=VECTOR ( 'NONE', #21490, 1000.000000000000000 ) ;
#12586=VERTEX_POINT ( 'NONE', #31479 ) ;
#12645=CARTESIAN_POINT ( 'NONE',  ( 9.000000000000001776, 0.000000000000000000, 0.000000000000000000 ) ) ;
#12668=DIRECTION ( 'NONE',  ( 0.8191520442889906883, 1.003171929053523391E-16, -0.5735764363510477137 ) ) ;
#12684=ORIENTED_EDGE ( 'NONE', *, *, #17599, .F. ) ;
#12694=CARTESIAN_POINT ( 'NONE',  ( 0.000000000000000000, 0.000000000000000000, -10.20000000000000462 ) ) ;
#12717=ORIENTED_EDGE ( 'NONE', *, *, #42112, .F. ) ;
#12739=EDGE_CURVE ( 'NONE', #12586, #70885, #10333, .T. ) ;
#12790=CARTESIAN_POINT ( 'NONE',  ( 9.000000000000000000, 5.196152422706648899, -0.8038475772933779684 ) ) ;
#12861=AXIS2_PLACEMENT_3D ( 'NONE', #22242, #45272, #5292 ) ;
#13050=DIRECTION ( 'NONE',  ( -0.000000000000000000, -0.000000000000000000, 1.000000000000000000 ) ) ;
#13128=FACE_OUTER_BOUND ( 'NONE', #65498, .T. ) ;
#13179=PLANE ( 'NONE',  #51848 ) ;
#13218=ORIENTED_EDGE ( 'NONE', *, *, #20370, .F. ) ;
#13400=CARTESIAN_POINT ( 'NONE',  ( 0.000000000000000000, 0.000000000000000000, -10.77459999999999951 ) ) ;
#13460=CARTESIAN_POINT ( 'NONE',  ( 0.000000000000000000, 0.000000000000000000, -10.80000000000000071 ) ) ;
#13478=DIRECTION ( 'NONE',  ( 0.8660254037844381525, 0.5000000000000008882, 0.000000000000000000 ) ) ;
#13615=AXIS2_PLACEMENT_3D ( 'NONE', #12694, #57632, #62894 ) ;
#13689=B_SPLINE_CURVE_WITH_KNOTS ( 'NONE', 3,
 ( #30345, #42392, #70347, #2044, #65408, #25031 ),
 .UNSPECIFIED., .F., .F.,
 ( 4, 2, 4 ),
 ( 2.380730968220417642E-07, 0.002629065763328348321, 0.005257893453559874149 ),
 .UNSPECIFIED. ) ;
#13802=VERTEX_POINT ( 'NONE', #62845 ) ;
#13872=ORIENTED_EDGE ( 'NONE', *, *, #58885, .T. ) ;
#13997=EDGE_CURVE ( 'NONE', #50322, #64865, #8120, .T. ) ;
#14000=( GEOMETRIC_REPRESENTATION_CONTEXT ( 3 ) GLOBAL_UNCERTAINTY_ASSIGNED_CONTEXT ( ( #7166 ) ) GLOBAL_UNIT_ASSIGNED_CONTEXT ( ( #1518, #24496, #18105 ) ) REPRESENTATION_CONTEXT ( 'NONE', 'WORKASPACE' ) );
#14047=CARTESIAN_POINT ( 'NONE',  ( 9.000000000000000000, 5.196152422706648899, -0.8038475772933779684 ) ) ;
#14145=ORIENTED_EDGE ( 'NONE', *, *, #45349, .F. ) ;
#14383=FACE_OUTER_BOUND ( 'NONE', #7194, .T. ) ;
#14450=AXIS2_PLACEMENT_3D ( 'NONE', #54435, #31408, #2743 ) ;
#14607=CARTESIAN_POINT ( 'NONE',  ( 4.500000000000013323, 7.794228634059940930, -10.20000000000000462 ) ) ;
#14645=EDGE_CURVE ( 'NONE', #4091, #8398, #60290, .T. ) ;
#14885=FACE_OUTER_BOUND ( 'NONE', #70077, .T. ) ;
#14994=DIRECTION ( 'NONE',  ( -0.8660254037844380415, -0.5000000000000012212, 0.000000000000000000 ) ) ;
#15032=ORIENTED_EDGE ( 'NONE', *, *, #70153, .T. ) ;
#15135=LINE ( 'NONE', #36038, #23703 ) ;
#15252=CARTESIAN_POINT ( 'NONE',  ( -9.000000000000000000, -5.196152422706644458, -10.80000000000000071 ) ) ;
#15381=EDGE_LOOP ( 'NONE', ( #7897, #16927, #10122, #68819, #49992, #49364 ) ) ;
#15405=DIRECTION ( 'NONE',  ( 1.000000000000000000, 0.000000000000000000, 0.000000000000000000 ) ) ;
#15408=CARTESIAN_POINT ( 'NONE',  ( -9.000000000000000000, 5.196152422706624918, -10.20000000000000284 ) ) ;
#15539=CARTESIAN_POINT ( 'NONE',  ( 0.7343025909353769753, -9.968355046870113867, -0.5590800469813878015 ) ) ;
#15731=FACE_OUTER_BOUND ( 'NONE', #42740, .T. ) ;
#15836=ORIENTED_EDGE ( 'NONE', *, *, #56536, .T. ) ;
#15843=ADVANCED_FACE ( 'NONE', ( #23621 ), #45872, .T. ) ;
#15871=CARTESIAN_POINT ( 'NONE',  ( 0.000000000000000000, 0.000000000000000000, -10.20000000000000462 ) ) ;
#15968=LINE ( 'NONE', #61258, #59069 ) ;
#15999=VERTEX_POINT ( 'NONE', #59079 ) ;
#16014=ORIENTED_EDGE ( 'NONE', *, *, #49092, .T. ) ;
#16146=AXIS2_PLACEMENT_3D ( 'NONE', #72754, #60298, #48606 ) ;
#16403=MANIFOLD_SOLID_BREP ( 'EndChamfer', #16557 ) ;
#16557=CLOSED_SHELL ( 'NONE', ( #1515, #28479, #37854, #40935, #59749, #49548, #27065, #54263, #47197, #59563, #60882, #23372, #46160, #23722, #48818, #3549, #2837, #38195, #57544, #55316, #59564, #73284, #57011, #15843, #50673, #36153, #7709, #30639, #54587, #17777 ) ) ;
#16613=VECTOR ( 'NONE', #14994, 999.9999999999998863 ) ;
#16640=CARTESIAN_POINT ( 'NONE',  ( -9.000000000000000000, 3.504753767550377930, -0.3593172728154441775 ) ) ;
#16818=AXIS2_PLACEMENT_3D ( 'NONE', #53603, #70216, #30213 ) ;
#16927=ORIENTED_EDGE ( 'NONE', *, *, #11791, .T. ) ;
#17013=CARTESIAN_POINT ( 'NONE',  ( 0.000000000000000000, 0.000000000000000000, 0.000000000000000000 ) ) ;
#17072=LINE ( 'NONE', #22348, #74204 ) ;
#17124=B_SPLINE_CURVE_WITH_KNOTS ( 'NONE', 3,
 ( #33231, #23373, #34351, #74312, #11318, #38874 ),
 .UNSPECIFIED., .F., .F.,
 ( 4, 2, 4 ),
 ( 2.380730968676944577E-07, 0.002629065763328393424, 0.005257893453559919252 ),
 .UNSPECIFIED. ) ;
#17413=CIRCLE ( 'NONE', #53543, 9.000000000000001776 ) ;
#17572=CARTESIAN_POINT ( 'NONE',  ( -4.500000000000007994, 7.794228634059939154, 0.000000000000000000 ) ) ;
#17599=EDGE_CURVE ( 'NONE', #47573, #62856, #30258, .T. ) ;
#17735=AXIS2_PLACEMENT_3D ( 'NONE', #40127, #46528, #49683 ) ;
#17777=ADVANCED_FACE ( 'NONE', ( #30779 ), #70410, .F. ) ;
#18022=ORIENTED_EDGE ( 'NONE', *, *, #26447, .F. ) ;
#18081=ORIENTED_EDGE ( 'NONE', *, *, #8892, .T. ) ;
#18105=( NAMED_UNIT ( * ) SI_UNIT ( $, .STERADIAN. ) SOLID_ANGLE_UNIT ( ) );
#18120=CARTESIAN_POINT ( 'NONE',  ( -9.000000000000000000, 5.196152422706624918, -10.20000000000000284 ) ) ;
#18189=ORIENTED_EDGE ( 'NONE', *, *, #59396, .F. ) ;
#18278=DIRECTION ( 'NONE',  ( -1.000000000000000000, 0.000000000000000000, 0.000000000000000000 ) ) ;
#18388=LINE ( 'NONE', #53093, #52406 ) ;
#18620=CARTESIAN_POINT ( 'NONE',  ( -6.024380653971853405, -6.914127053141861268, -0.09252763182293101407 ) ) ;
#18701=CARTESIAN_POINT ( 'NONE',  ( 9.000000000000000000, 5.196152422706622254, -10.20000000000000284 ) ) ;
#18705=EDGE_LOOP ( 'NONE', ( #46663, #56442, #71243 ) ) ;
#19112=ORIENTED_EDGE ( 'NONE', *, *, #14645, .F. ) ;
#19182=CARTESIAN_POINT ( 'NONE',  ( 0.000000000000000000, 0.000000000000000000, -10.14441321561125520 ) ) ;
#19190=ORIENTED_EDGE ( 'NONE', *, *, #27269, .T. ) ;
#19254=PLANE ( 'NONE',  #67729 ) ;
#19717=CIRCLE ( 'NONE', #22083, 8.999999999999998224 ) ;
#19857=VERTEX_POINT ( 'NONE', #10906 ) ;
#19906=CYLINDRICAL_SURFACE ( 'NONE', #68903, 5.099999999999999645 ) ;
#19923=ORIENTED_EDGE ( 'NONE', *, *, #66150, .T. ) ;
#19954=LINE ( 'NONE', #15408, #1869 ) ;
#20073=CARTESIAN_POINT ( 'NONE',  ( -4.076600168545496672E-14, -10.39230484541327471, -0.8038475772933779684 ) ) ;
#20207=VECTOR ( 'NONE', #63162, 1000.000000000000000 ) ;
#20223=AXIS2_PLACEMENT_3D ( 'NONE', #26194, #31006, #53296 ) ;
#20307=B_SPLINE_CURVE_WITH_KNOTS ( 'NONE', 3,
 ( #12205, #59991, #65648, #7944, #71301, #37358 ),
 .UNSPECIFIED., .F., .F.,
 ( 4, 2, 4 ),
 ( 2.380730968267134156E-07, 0.002629065763328368270, 0.005257893453559909711 ),
 .UNSPECIFIED. ) ;
#20370=EDGE_CURVE ( 'NONE', #72372, #25774, #36885, .T. ) ;
#20417=DIRECTION ( 'NONE',  ( -1.000000000000000000, 0.000000000000000000, 0.000000000000000000 ) ) ;
#20520=CARTESIAN_POINT ( 'NONE',  ( 0.000000000000000000, 0.000000000000000000, -0.6301867843887376530 ) ) ;
#20539=DIRECTION ( 'NONE',  ( 0.000000000000000000, 0.000000000000000000, 1.000000000000000000 ) ) ;
#20540=ORIENTED_EDGE ( 'NONE', *, *, #35871, .F. ) ;
#20614=CIRCLE ( 'NONE', #72443, 6.000000000000000000 ) ;
#20663=FACE_BOUND ( 'NONE', #45072, .T. ) ;
#20673=EDGE_LOOP ( 'NONE', ( #58619, #36547, #54194 ) ) ;
#20677=ORIENTED_EDGE ( 'NONE', *, *, #44825, .T. ) ;
#20875=ORIENTED_EDGE ( 'NONE', *, *, #7090, .F. ) ;
#21097=DIRECTION ( 'NONE',  ( 0.000000000000000000, 0.000000000000000000, 1.000000000000000000 ) ) ;
#21151=ORIENTED_EDGE ( 'NONE', *, *, #68754, .T. ) ;
#21205=CARTESIAN_POINT ( 'NONE',  ( 2.975619346028165246, -8.674330214978068554, -0.09252763182293416433 ) ) ;
#21438=ORIENTED_EDGE ( 'NONE', *, *, #73161, .F. ) ;
#21490=DIRECTION ( 'NONE',  ( 0.000000000000000000, -1.000000000000000000, 0.000000000000000000 ) ) ;
#21615=CARTESIAN_POINT ( 'NONE',  ( 0.000000000000000000, 0.000000000000000000, -10.20000000000000462 ) ) ;
#21654=EDGE_CURVE ( 'NONE', #71873, #44162, #27483, .T. ) ;
#21674=LINE ( 'NONE', #10371, #27725 ) ;
#22007=CARTESIAN_POINT ( 'NONE',  ( -9.000000000000000000, 5.196152422706624918, -0.8038475772933814101 ) ) ;
#22070=ORIENTED_EDGE ( 'NONE', *, *, #68348, .F. ) ;
#22083=AXIS2_PLACEMENT_3D ( 'NONE', #58990, #30303, #1284 ) ;
#22158=ORIENTED_EDGE ( 'NONE', *, *, #3252, .T. ) ;
#22242=CARTESIAN_POINT ( 'NONE',  ( 0.000000000000000000, 20.39230484541327471, -10.20000000000000284 ) ) ;
#22295=DIRECTION ( 'NONE',  ( -0.000000000000000000, -0.000000000000000000, 1.000000000000000000 ) ) ;
#22348=CARTESIAN_POINT ( 'NONE',  ( -9.000000000000000000, 5.196152422706624918, -10.20000000000000284 ) ) ;
#22410=EDGE_CURVE ( 'NONE', #63061, #71873, #39092, .T. ) ;
#22463=CARTESIAN_POINT ( 'NONE',  ( 9.000000000000001776, -5.196152422706648899, -0.8038475772933779684 ) ) ;
#22586=DIRECTION ( 'NONE',  ( 1.000000000000000000, 0.000000000000000000, 0.000000000000000000 ) ) ;
#22653=CIRCLE ( 'NONE', #20223, 6.000000000000000000 ) ;
#22679=CARTESIAN_POINT ( 'NONE',  ( -9.000000000000001776, 0.8785859941773058734, -1.113001292692150251E-15 ) ) ;
#22763=DIRECTION ( 'NONE',  ( -0.8191520442889924647, 1.003171929053525486E-16, 0.5735764363510451602 ) ) ;
#22856=CARTESIAN_POINT ( 'NONE',  ( -5.266666970006217419, 7.351593252548062729, 4.363913744254155347E-15 ) ) ;
#22863=SHAPE_REPRESENTATION ( 'hexagon nut style 1_is_IS 1364-3 - M12-W-N', ( #57354 ), #14000 ) ;
#22890=ORIENTED_EDGE ( 'NONE', *, *, #66727, .T. ) ;
#22900=ORIENTED_EDGE ( 'NONE', *, *, #23779, .T. ) ;
#22927=CIRCLE ( 'NONE', #2470, 5.099999999999999645 ) ;
#22953=CARTESIAN_POINT ( 'NONE',  ( 6.000000000000000000, 0.000000000000000000, -25.03750572909317285 ) ) ;
#23177=VERTEX_POINT ( 'NONE', #22007 ) ;
#23345=DIRECTION ( 'NONE',  ( 1.000000000000000000, 0.000000000000000000, 0.000000000000000000 ) ) ;
#23372=ADVANCED_FACE ( 'NONE', ( #66836 ), #65703, .T. ) ;
#23373=CARTESIAN_POINT ( 'NONE',  ( -0.7361406979141749130, -9.967293815311105476, -0.5584673446549270892 ) ) ;
#23597=PLANE ( 'NONE',  #63739 ) ;
#23604=CARTESIAN_POINT ( 'NONE',  ( -8.263859302085863945, 5.621163452808790595, -0.5584673446549202058 ) ) ;
#23621=FACE_OUTER_BOUND ( 'NONE', #18705, .T. ) ;
#23703=VECTOR ( 'NONE', #53017, 1000.000000000000000 ) ;
#23722=ADVANCED_FACE ( 'NONE', ( #50049, #73065 ), #6180, .T. ) ;
#23779=EDGE_CURVE ( 'NONE', #27106, #56231, #46669, .T. ) ;
#24127=ORIENTED_EDGE ( 'NONE', *, *, #55402, .F. ) ;
#24259=FACE_OUTER_BOUND ( 'NONE', #30455, .T. ) ;
#24264=EDGE_CURVE ( 'NONE', #64865, #23177, #72545, .T. ) ;
#24337=LINE ( 'NONE', #2441, #50605 ) ;
#24368=DIRECTION ( 'NONE',  ( 0.000000000000000000, 0.000000000000000000, 1.000000000000000000 ) ) ;
#24407=ORIENTED_EDGE ( 'NONE', *, *, #668, .F. ) ;
#24496=( NAMED_UNIT ( * ) PLANE_ANGLE_UNIT ( ) SI_UNIT ( $, .RADIAN. ) );
#24543=DIRECTION ( 'NONE',  ( -0.000000000000000000, -0.000000000000000000, 1.000000000000000000 ) ) ;
#24570=FACE_OUTER_BOUND ( 'NONE', #38359, .T. ) ;
#24713=CARTESIAN_POINT ( 'NONE',  ( -4.500000000000010658, -7.794228634059939154, 0.000000000000000000 ) ) ;
#24858=ORIENTED_EDGE ( 'NONE', *, *, #29122, .F. ) ;
#25031=CARTESIAN_POINT ( 'NONE',  ( 4.500000000000006217, -7.794228634059941818, 0.000000000000000000 ) ) ;
#25108=DIRECTION ( 'NONE',  ( -0.000000000000000000, -0.000000000000000000, 1.000000000000000000 ) ) ;
#25271=AXIS2_PLACEMENT_3D ( 'NONE', #72104, #49848, #20417 ) ;
#25376=AXIS2_PLACEMENT_3D ( 'NONE', #15871, #4574, #27572 ) ;
#25478=DIRECTION ( 'NONE',  ( 1.000000000000000000, 0.000000000000000000, 0.000000000000000000 ) ) ;
#25540=FACE_OUTER_BOUND ( 'NONE', #20673, .T. ) ;
#25565=ORIENTED_EDGE ( 'NONE', *, *, #45349, .T. ) ;
#25763=PRODUCT ( 'hexagon nut style 1_is_IS 1364-3 - M12-W-N', 'hexagon nut style 1_is_IS 1364-3 - M12-W-N', '', ( #71248 ) ) ;
#25774=VERTEX_POINT ( 'NONE', #43572 ) ;
#25807=ORIENTED_EDGE ( 'NONE', *, *, #35656, .F. ) ;
#25836=EDGE_LOOP ( 'NONE', ( #20677, #48661, #66001, #36884, #19923, #68304 ) ) ;
#25870=EDGE_CURVE ( 'NONE', #25774, #327, #5461, .T. ) ;
#25880=CARTESIAN_POINT ( 'NONE',  ( -4.500000000000007994, 7.794228634059939154, 0.000000000000000000 ) ) ;
#25994=DIRECTION ( 'NONE',  ( 0.000000000000000000, -0.000000000000000000, 1.000000000000000000 ) ) ;
#26194=CARTESIAN_POINT ( 'NONE',  ( 0.000000000000000000, 0.000000000000000000, 0.000000000000000000 ) ) ;
#26269=ORIENTED_EDGE ( 'NONE', *, *, #24264, .F. ) ;
#26288=DIRECTION ( 'NONE',  ( 0.000000000000000000, -0.000000000000000000, 1.000000000000000000 ) ) ;
#26315=VECTOR ( 'NONE', #45961, 1000.000000000000000 ) ;
#26353=AXIS2_PLACEMENT_3D ( 'NONE', #47575, #35541, #46845 ) ;
#26447=EDGE_CURVE ( 'NONE', #63061, #59993, #54110, .T. ) ;
#26480=CARTESIAN_POINT ( 'NONE',  ( 2.598723904613009950, -8.891930899535452681, -0.1469846612282645348 ) ) ;
#26523=DIRECTION ( 'NONE',  ( 1.000000000000000000, 0.000000000000000000, 0.000000000000000000 ) ) ;
#26695=DIRECTION ( 'NONE',  ( 0.000000000000000000, 0.000000000000000000, 1.000000000000000000 ) ) ;
#26738=DIRECTION ( 'NONE',  ( 0.000000000000000000, -1.000000000000000000, 0.000000000000000000 ) ) ;
#26821=ORIENTED_EDGE ( 'NONE', *, *, #69688, .T. ) ;
#26838=DIRECTION ( 'NONE',  ( -1.000000000000000000, 0.000000000000000000, 0.000000000000000000 ) ) ;
#26977=EDGE_CURVE ( 'NONE', #41903, #57937, #7599, .T. ) ;
#27065=ADVANCED_FACE ( 'NONE', ( #24570 ), #29873, .T. ) ;
#27106=VERTEX_POINT ( 'NONE', #69041 ) ;
#27269=EDGE_CURVE ( 'NONE', #13802, #31722, #49895, .T. ) ;
#27478=CARTESIAN_POINT ( 'NONE',  ( 0.000000000000000000, 0.000000000000000000, -10.20000000000000462 ) ) ;
#27483=CIRCLE ( 'NONE', #8052, 6.000000000000000000 ) ;
#27566=ORIENTED_EDGE ( 'NONE', *, *, #73700, .F. ) ;
#27572=DIRECTION ( 'NONE',  ( 1.000000000000000000, 0.000000000000000000, 0.000000000000000000 ) ) ;
#27663=AXIS2_PLACEMENT_3D ( 'NONE', #73089, #61020, #73458 ) ;
#27725=VECTOR ( 'NONE', #32654, 999.9999999999998863 ) ;
#27987=VECTOR ( 'NONE', #22763, 1000.000000000000000 ) ;
#28103=B_SPLINE_CURVE_WITH_KNOTS ( 'NONE', 3,
 ( #59353, #30670, #55186, #21205, #26480, #54808, #15539, #20073 ),
 .UNSPECIFIED., .F., .F.,
 ( 4, 2, 2, 4 ),
 ( 0.005257893453559874149, 0.006567392922673220834, 0.007876892391786566652, 0.01049589133001326002 ),
 .UNSPECIFIED. ) ;
#28150=DIRECTION ( 'NONE',  ( 0.000000000000000000, 0.000000000000000000, 1.000000000000000000 ) ) ;
#28227=ORIENTED_EDGE ( 'NONE', *, *, #55900, .T. ) ;
#28316=DIRECTION ( 'NONE',  ( -0.000000000000000000, -0.000000000000000000, 1.000000000000000000 ) ) ;
#28451=( LENGTH_UNIT ( ) NAMED_UNIT ( * ) SI_UNIT ( .MILLI., .METRE. ) );
#28479=ADVANCED_FACE ( 'NONE', ( #15731 ), #10763, .F. ) ;
#28908=ORIENTED_EDGE ( 'NONE', *, *, #55900, .F. ) ;
#29093=ORIENTED_EDGE ( 'NONE', *, *, #72837, .T. ) ;
#29122=EDGE_CURVE ( 'NONE', #30116, #61426, #21674, .T. ) ;
#29258=CIRCLE ( 'NONE', #30440, 9.000000000000001776 ) ;
#29421=CARTESIAN_POINT ( 'NONE',  ( 5.265513565426386933, 7.352259170992713422, -0.01899995639453637419 ) ) ;
#29480=CYLINDRICAL_SURFACE ( 'NONE', #48116, 9.000000000000001776 ) ;
#29495=EDGE_CURVE ( 'NONE', #69396, #23177, #24337, .T. ) ;
#29569=FACE_OUTER_BOUND ( 'NONE', #31918, .T. ) ;
#29604=VECTOR ( 'NONE', #50169, 1000.000000000000000 ) ;
#29832=DIRECTION ( 'NONE',  ( -1.000000000000000000, 0.000000000000000000, 0.000000000000000000 ) ) ;
#29873=PLANE ( 'NONE',  #26353 ) ;
#29940=CARTESIAN_POINT ( 'NONE',  ( -9.000000000000000000, -5.196152422706648899, -0.8038475772933779684 ) ) ;
#30012=EDGE_LOOP ( 'NONE', ( #4925, #50931, #19190, #21438, #58781, #22158 ) ) ;
#30067=EDGE_LOOP ( 'NONE', ( #55150, #9747, #69140, #47964 ) ) ;
#30116=VERTEX_POINT ( 'NONE', #18701 ) ;
#30213=DIRECTION ( 'NONE',  ( -1.000000000000000000, 1.776356839400250465E-15, 0.000000000000000000 ) ) ;
#30258=CIRCLE ( 'NONE', #41141, 5.099999999999999645 ) ;
#30303=DIRECTION ( 'NONE',  ( -0.000000000000000000, -0.000000000000000000, 1.000000000000000000 ) ) ;
#30345=CARTESIAN_POINT ( 'NONE',  ( 9.000000000000001776, -5.196152422706648899, -0.8038475772933779684 ) ) ;
#30363=VECTOR ( 'NONE', #13478, 1000.000000000000000 ) ;
#30440=AXIS2_PLACEMENT_3D ( 'NONE', #58263, #34514, #39766 ) ;
#30455=EDGE_LOOP ( 'NONE', ( #60930, #15032, #39762, #58330 ) ) ;
#30553=CARTESIAN_POINT ( 'NONE',  ( 0.000000000000000000, 20.39230484541327471, -10.20000000000000284 ) ) ;
#30626=ORIENTED_EDGE ( 'NONE', *, *, #68581, .F. ) ;
#30639=ADVANCED_FACE ( 'NONE', ( #24259 ), #3653, .F. ) ;
#30670=CARTESIAN_POINT ( 'NONE',  ( 4.118099735505524883, -8.014718854569444773, -6.906706651911562598E-15 ) ) ;
#30702=EDGE_CURVE ( 'NONE', #4091, #61956, #28103, .T. ) ;
#30756=CARTESIAN_POINT ( 'NONE',  ( -4.500000000000022204, -7.794228634059960470, -10.20000000000000462 ) ) ;
#30779=FACE_OUTER_BOUND ( 'NONE', #70322, .T. ) ;
#30867=EDGE_CURVE ( 'NONE', #59993, #63061, #22927, .T. ) ;
#30914=DIRECTION ( 'NONE',  ( -1.000000000000000000, 0.000000000000000000, -0.000000000000000000 ) ) ;
#30946=FACE_OUTER_BOUND ( 'NONE', #15381, .T. ) ;
#31006=DIRECTION ( 'NONE',  ( -0.000000000000000000, -0.000000000000000000, 1.000000000000000000 ) ) ;
#31200=DIRECTION ( 'NONE',  ( 0.000000000000000000, -0.000000000000000000, 1.000000000000000000 ) ) ;
#31215=CARTESIAN_POINT ( 'NONE',  ( 0.000000000000000000, 0.000000000000000000, 0.000000000000000000 ) ) ;
#31225=VECTOR ( 'NONE', #52887, 999.9999999999997726 ) ;
#31272=EDGE_LOOP ( 'NONE', ( #65291, #6649, #7779, #48278, #26821, #21151 ) ) ;
#31408=DIRECTION ( 'NONE',  ( -0.000000000000000000, -0.000000000000000000, 1.000000000000000000 ) ) ;
#31417=CARTESIAN_POINT ( 'NONE',  ( 9.000000000000000000, 1.769118300197576321, -0.07756262466202530625 ) ) ;
#31479=CARTESIAN_POINT ( 'NONE',  ( 1.334622868157815783E-15, 10.39230484541327293, -10.20000000000000284 ) ) ;
#31491=STYLED_ITEM('',(#74706),#16403);
#31565=CARTESIAN_POINT ( 'NONE',  ( -5.099999999999999645, 6.245698675651499853E-16, -10.14441321561125520 ) ) ;
#31595=CARTESIAN_POINT ( 'NONE',  ( -1.001543065824775909E-15, -10.39230484541329247, -10.20000000000000284 ) ) ;
#31683=ORIENTED_EDGE ( 'NONE', *, *, #5787, .T. ) ;
#31722=VERTEX_POINT ( 'NONE', #14047 ) ;
#31918=EDGE_LOOP ( 'NONE', ( #63755, #3405, #24858 ) ) ;
#32076=CARTESIAN_POINT ( 'NONE',  ( -5.265513565426391374, -7.352259170992729409, -0.01899995639454697682 ) ) ;
#32283=EDGE_LOOP ( 'NONE', ( #4329, #60468, #33540 ) ) ;
#32414=PLANE ( 'NONE',  #1042 ) ;
#32459=CARTESIAN_POINT ( 'NONE',  ( -8.265697409064609147, -5.620102221249831942, -0.5590800469813734797 ) ) ;
#32609=DIRECTION ( 'NONE',  ( 0.000000000000000000, 0.000000000000000000, -1.000000000000000000 ) ) ;
#32654=DIRECTION ( 'NONE',  ( -0.8660254037844379305, 0.5000000000000014433, 0.000000000000000000 ) ) ;
#32832=VECTOR ( 'NONE', #42920, 999.9999999999998863 ) ;
#32929=DIRECTION ( 'NONE',  ( -0.000000000000000000, -0.000000000000000000, 1.000000000000000000 ) ) ;
#32941=FACE_OUTER_BOUND ( 'NONE', #72468, .T. ) ;
#33089=CARTESIAN_POINT ( 'NONE',  ( 5.204170427930421283E-15, 10.39230484541327293, -0.8038475772933779684 ) ) ;
#33119=ORIENTED_EDGE ( 'NONE', *, *, #68348, .T. ) ;
#33202=DIRECTION ( 'NONE',  ( -0.000000000000000000, -0.000000000000000000, 1.000000000000000000 ) ) ;
#33231=CARTESIAN_POINT ( 'NONE',  ( -4.076600168545496672E-14, -10.39230484541327471, -0.8038475772933779684 ) ) ;
#33236=CIRCLE ( 'NONE', #36827, 6.000000000000000000 ) ;
#33358=DIRECTION ( 'NONE',  ( 0.000000000000000000, 0.000000000000000000, 1.000000000000000000 ) ) ;
#33540=ORIENTED_EDGE ( 'NONE', *, *, #35808, .F. ) ;
#33707=APPLICATION_CONTEXT ( 'automotive_design' ) ;
#33794=EDGE_CURVE ( 'NONE', #15999, #69396, #9734, .T. ) ;
#34201=ORIENTED_EDGE ( 'NONE', *, *, #62121, .T. ) ;
#34254=EDGE_LOOP ( 'NONE', ( #73859, #72844, #42878, #66628, #18081, #35708 ) ) ;
#34351=CARTESIAN_POINT ( 'NONE',  ( -1.477658550686901773, -9.539178283403858316, -0.3563104543936471691 ) ) ;
#34371=ORIENTED_EDGE ( 'NONE', *, *, #58885, .F. ) ;
#34409=CARTESIAN_POINT ( 'NONE',  ( -9.000000000000000000, 5.196152422706624918, -0.8038475772933814101 ) ) ;
#34459=DIRECTION ( 'NONE',  ( 1.000000000000000000, 0.000000000000000000, 0.000000000000000000 ) ) ;
#34514=DIRECTION ( 'NONE',  ( -0.000000000000000000, -0.000000000000000000, 1.000000000000000000 ) ) ;
#34544=B_SPLINE_CURVE_WITH_KNOTS ( 'NONE', 3,
 ( #41334, #23604, #58331, #70011, #22856, #17572 ),
 .UNSPECIFIED., .F., .F.,
 ( 4, 2, 4 ),
 ( 2.380730968220572225E-07, 0.002629065763328352658, 0.005257893453559882822 ),
 .UNSPECIFIED. ) ;
#34570=CARTESIAN_POINT ( 'NONE',  ( 1.334622868157815783E-15, 10.39230484541327293, -10.20000000000000284 ) ) ;
#34898=EDGE_CURVE ( 'NONE', #27106, #44162, #4491, .T. ) ;
#34946=CARTESIAN_POINT ( 'NONE',  ( 9.000000000000000000, 5.196152422706622254, -10.80000000000000071 ) ) ;
#34950=LINE ( 'NONE', #12645, #48460 ) ;
#35253=ORIENTED_EDGE ( 'NONE', *, *, #59396, .T. ) ;
#35279=DIRECTION ( 'NONE',  ( 0.000000000000000000, -0.000000000000000000, 1.000000000000000000 ) ) ;
#35345=LINE ( 'NONE', #59452, #50858 ) ;
#35541=DIRECTION ( 'NONE',  ( -0.5000000000000011102, 0.8660254037844380415, 0.000000000000000000 ) ) ;
#35656=EDGE_CURVE ( 'NONE', #23177, #63081, #34544, .T. ) ;
#35708=ORIENTED_EDGE ( 'NONE', *, *, #55402, .T. ) ;
#35808=EDGE_CURVE ( 'NONE', #57937, #72372, #70398, .T. ) ;
#35822=CARTESIAN_POINT ( 'NONE',  ( 8.265697409064602041, 5.620102221249814178, -0.5590800469813634876 ) ) ;
#35871=EDGE_CURVE ( 'NONE', #59993, #44162, #48105, .T. ) ;
#35965=AXIS2_PLACEMENT_3D ( 'NONE', #72023, #21097, #50510 ) ;
#36038=CARTESIAN_POINT ( 'NONE',  ( 9.000000000000000000, 5.196152422706622254, -10.20000000000000284 ) ) ;
#36153=ADVANCED_FACE ( 'NONE', ( #14885 ), #59776, .T. ) ;
#36156=DIRECTION ( 'NONE',  ( -0.000000000000000000, -0.000000000000000000, 1.000000000000000000 ) ) ;
#36472=AXIS2_PLACEMENT_3D ( 'NONE', #54995, #26288, #59896 ) ;
#36547=ORIENTED_EDGE ( 'NONE', *, *, #13997, .F. ) ;
#36625=CARTESIAN_POINT ( 'NONE',  ( 4.500000000000017764, -7.794228634059961358, -10.20000000000000462 ) ) ;
#36627=LINE ( 'NONE', #70223, #61747 ) ;
#36684=EDGE_CURVE ( 'NONE', #8398, #31722, #62299, .T. ) ;
#36803=CARTESIAN_POINT ( 'NONE',  ( -1.001543065824775909E-15, -10.39230484541329247, -10.20000000000000284 ) ) ;
#36827=AXIS2_PLACEMENT_3D ( 'NONE', #37940, #25108, #25478 ) ;
#36833=AXIS2_PLACEMENT_3D ( 'NONE', #21615, #72176, #26523 ) ;
#36869=EDGE_LOOP ( 'NONE', ( #35253, #62039, #8529 ) ) ;
#36884=ORIENTED_EDGE ( 'NONE', *, *, #8536, .F. ) ;
#36885=LINE ( 'NONE', #31595, #30363 ) ;
#36902=DIRECTION ( 'NONE',  ( 0.000000000000000000, 0.000000000000000000, 1.000000000000000000 ) ) ;
#37132=CIRCLE ( 'NONE', #69687, 9.000000000000001776 ) ;
#37133=DIRECTION ( 'NONE',  ( -1.000000000000000000, 0.000000000000000000, -0.000000000000000000 ) ) ;
#37189=ORIENTED_EDGE ( 'NONE', *, *, #12739, .F. ) ;
#37358=CARTESIAN_POINT ( 'NONE',  ( 4.500000000000010658, 7.794228634059937377, 0.000000000000000000 ) ) ;
#37540=ORIENTED_EDGE ( 'NONE', *, *, #66150, .F. ) ;
#37674=CONICAL_SURFACE ( 'NONE', #61744, 8.999999999999998224, 1.047197551196595855 ) ;
#37854=ADVANCED_FACE ( 'NONE', ( #51110 ), #6850, .F. ) ;
#37915=LINE ( 'NONE', #15252, #52263 ) ;
#37924=DIRECTION ( 'NONE',  ( 0.000000000000000000, 0.000000000000000000, -1.000000000000000000 ) ) ;
#37940=CARTESIAN_POINT ( 'NONE',  ( 0.000000000000000000, 0.000000000000000000, 0.000000000000000000 ) ) ;
#38040=EDGE_CURVE ( 'NONE', #61956, #41819, #17124, .T. ) ;
#38195=ADVANCED_FACE ( 'NONE', ( #56978 ), #62615, .T. ) ;
#38293=EDGE_LOOP ( 'NONE', ( #28908, #40246, #8490, #24407, #40609, #1957 ) ) ;
#38359=EDGE_LOOP ( 'NONE', ( #47230, #69132, #22890, #37189, #41467, #4976 ) ) ;
#38622=EDGE_CURVE ( 'NONE', #47573, #6721, #44042, .T. ) ;
#38683=CARTESIAN_POINT ( 'NONE',  ( -9.000000000000000000, -5.196152422706648899, -0.8038475772933779684 ) ) ;
#38736=CARTESIAN_POINT ( 'NONE',  ( -0.7343025909353899650, 9.968355046870078340, -0.5590800469813719253 ) ) ;
#38780=FACE_OUTER_BOUND ( 'NONE', #40228, .T. ) ;
#38874=CARTESIAN_POINT ( 'NONE',  ( -4.500000000000010658, -7.794228634059939154, 0.000000000000000000 ) ) ;
#39092=LINE ( 'NONE', #10417, #46611 ) ;
#39253=CIRCLE ( 'NONE', #36833, 9.000000000000001776 ) ;
#39404=ORIENTED_EDGE ( 'NONE', *, *, #5787, .F. ) ;
#39469=FACE_OUTER_BOUND ( 'NONE', #30012, .T. ) ;
#39596=CARTESIAN_POINT ( 'NONE',  ( 9.000000000000000000, 5.196152422706622254, -10.20000000000000284 ) ) ;
#39667=VERTEX_POINT ( 'NONE', #231 ) ;
#39762=ORIENTED_EDGE ( 'NONE', *, *, #38622, .T. ) ;
#39766=DIRECTION ( 'NONE',  ( 1.000000000000000000, 0.000000000000000000, 0.000000000000000000 ) ) ;
#39810=ORIENTED_EDGE ( 'NONE', *, *, #35871, .T. ) ;
#39821=ORIENTED_EDGE ( 'NONE', *, *, #3252, .F. ) ;
#39834=DIRECTION ( 'NONE',  ( -0.8660254037844379305, 0.5000000000000014433, 0.000000000000000000 ) ) ;
#39853=CARTESIAN_POINT ( 'NONE',  ( -9.000000000000001776, 1.102182119232617911E-15, -10.80000000000000071 ) ) ;
#40127=CARTESIAN_POINT ( 'NONE',  ( 0.000000000000000000, 0.000000000000000000, -10.80000000000000071 ) ) ;
#40156=EDGE_LOOP ( 'NONE', ( #45515, #33119, #47117, #57624, #61811, #73441 ) ) ;
#40157=CARTESIAN_POINT ( 'NONE',  ( 9.000000000000000000, -5.196152422706648011, -10.80000000000000071 ) ) ;
#40212=DIRECTION ( 'NONE',  ( -0.000000000000000000, -0.000000000000000000, 1.000000000000000000 ) ) ;
#40228=EDGE_LOOP ( 'NONE', ( #26269, #58386, #25807 ) ) ;
#40246=ORIENTED_EDGE ( 'NONE', *, *, #25870, .F. ) ;
#40375=CARTESIAN_POINT ( 'NONE',  ( 0.000000000000000000, -10.39230484541329247, -10.20000000000000284 ) ) ;
#40606=CARTESIAN_POINT ( 'NONE',  ( 0.000000000000000000, 0.000000000000000000, 0.000000000000000000 ) ) ;
#40609=ORIENTED_EDGE ( 'NONE', *, *, #73161, .T. ) ;
#40809=AXIS2_PLACEMENT_3D ( 'NONE', #64540, #7200, #53224 ) ;
#40935=ADVANCED_FACE ( 'NONE', ( #67226 ), #67965, .T. ) ;
#41126=PRODUCT_DEFINITION_CONTEXT ( 'detailed design', #52979, 'design' ) ;
#41141=AXIS2_PLACEMENT_3D ( 'NONE', #61297, #55651, #3967 ) ;
#41334=CARTESIAN_POINT ( 'NONE',  ( -9.000000000000000000, 5.196152422706624918, -0.8038475772933814101 ) ) ;
#41467=ORIENTED_EDGE ( 'NONE', *, *, #66888, .T. ) ;
#41500=DIRECTION ( 'NONE',  ( 0.000000000000000000, 0.000000000000000000, -1.000000000000000000 ) ) ;
#41562=B_SPLINE_CURVE_WITH_KNOTS ( 'NONE', 3,
 ( #10052, #50035, #62100, #68503, #61359, #10423, #38736, #33089 ),
 .UNSPECIFIED., .F., .F.,
 ( 4, 2, 2, 4 ),
 ( 0.005257893453559882822, 0.006567392922673223436, 0.007876892391786564918, 0.01049589133001324268 ),
 .UNSPECIFIED. ) ;
#41693=DIRECTION ( 'NONE',  ( 0.000000000000000000, 0.000000000000000000, -1.000000000000000000 ) ) ;
#41735=CARTESIAN_POINT ( 'NONE',  ( 0.000000000000000000, 0.000000000000000000, -25.03750572909317285 ) ) ;
#41742=LINE ( 'NONE', #64752, #63129 ) ;
#41802=EDGE_LOOP ( 'NONE', ( #22900, #8683 ) ) ;
#41815=DIRECTION ( 'NONE',  ( 1.000000000000000000, 0.000000000000000000, 0.000000000000000000 ) ) ;
#41819=VERTEX_POINT ( 'NONE', #24713 ) ;
#41849=SHAPE_REPRESENTATION_RELATIONSHIP ( 'NONE' , 'NONE' ,  #22863, #5729 ) ;
#41903=VERTEX_POINT ( 'NONE', #30756 ) ;
#42112=EDGE_CURVE ( 'NONE', #6721, #19857, #22653, .T. ) ;
#42392=CARTESIAN_POINT ( 'NONE',  ( 8.263859302085865721, -5.621163452808815464, -0.5584673446549284215 ) ) ;
#42427=CARTESIAN_POINT ( 'NONE',  ( -9.000000000000000000, -0.8780643052077380384, -9.046311876675927621E-16 ) ) ;
#42583=SHAPE_DEFINITION_REPRESENTATION ( #65518, #22863 ) ;
#42600=DIRECTION ( 'NONE',  ( 0.000000000000000000, 0.000000000000000000, -1.000000000000000000 ) ) ;
#42609=FACE_OUTER_BOUND ( 'NONE', #38293, .T. ) ;
#42636=CARTESIAN_POINT ( 'NONE',  ( 0.000000000000000000, 20.39230484541327471, -10.20000000000000284 ) ) ;
#42691=CARTESIAN_POINT ( 'NONE',  ( -9.000000000000000000, 5.196152422706624918, -10.80000000000000071 ) ) ;
#42740=EDGE_LOOP ( 'NONE', ( #53521, #39810, #49937, #66482 ) ) ;
#42878=ORIENTED_EDGE ( 'NONE', *, *, #2080, .T. ) ;
#42920=DIRECTION ( 'NONE',  ( -0.8660254037844379305, 0.5000000000000014433, 0.000000000000000000 ) ) ;
#42987=PRODUCT_DEFINITION_FORMATION_WITH_SPECIFIED_SOURCE ( 'ANY', '', #25763, .NOT_KNOWN. ) ;
#43092=CARTESIAN_POINT ( 'NONE',  ( 4.500000000000006217, -7.794228634059941818, 0.000000000000000000 ) ) ;
#43098=CARTESIAN_POINT ( 'NONE',  ( 9.000000000000000000, 3.504753767550392585, -0.3593172728154473972 ) ) ;
#43218=CIRCLE ( 'NONE', #51627, 9.000000000000001776 ) ;
#43572=CARTESIAN_POINT ( 'NONE',  ( 9.000000000000000000, -5.196152422706648011, -10.20000000000000284 ) ) ;
#43679=LINE ( 'NONE', #72731, #32832 ) ;
#43680=CARTESIAN_POINT ( 'NONE',  ( 1.334622868157815783E-15, 10.39230484541327293, -10.20000000000000284 ) ) ;
#43986=VECTOR ( 'NONE', #45860, 999.9999999999998863 ) ;
#44016=EDGE_CURVE ( 'NONE', #62856, #19857, #904, .T. ) ;
#44042=LINE ( 'NONE', #50068, #53854 ) ;
#44120=CARTESIAN_POINT ( 'NONE',  ( 9.000000000000000000, 0.000000000000000000, -10.20000000000000462 ) ) ;
#44162=VERTEX_POINT ( 'NONE', #58805 ) ;
#44255=AXIS2_PLACEMENT_3D ( 'NONE', #5431, #69172, #44395 ) ;
#44395=DIRECTION ( 'NONE',  ( -1.000000000000000000, 0.000000000000000000, 0.000000000000000000 ) ) ;
#44614=DIRECTION ( 'NONE',  ( 0.000000000000000000, 0.000000000000000000, -1.000000000000000000 ) ) ;
#44825=EDGE_CURVE ( 'NONE', #57937, #61956, #35345, .T. ) ;
#45072=EDGE_LOOP ( 'NONE', ( #12717, #27566 ) ) ;
#45074=CIRCLE ( 'NONE', #8881, 8.999999999999998224 ) ;
#45272=DIRECTION ( 'NONE',  ( 0.000000000000000000, 0.000000000000000000, -1.000000000000000000 ) ) ;
#45349=EDGE_CURVE ( 'NONE', #56231, #71873, #36627, .T. ) ;
#45350=AXIS2_PLACEMENT_3D ( 'NONE', #73368, #37924, #2839 ) ;
#45515=ORIENTED_EDGE ( 'NONE', *, *, #25870, .T. ) ;
#45563=CARTESIAN_POINT ( 'NONE',  ( 9.000000000000000000, -1.750439824713163617, -0.07547478993377551570 ) ) ;
#45662=CARTESIAN_POINT ( 'NONE',  ( 0.000000000000000000, 0.000000000000000000, -10.77459999999999951 ) ) ;
#45860=DIRECTION ( 'NONE',  ( -0.8660254037844380415, -0.5000000000000012212, 0.000000000000000000 ) ) ;
#45872=CONICAL_SURFACE ( 'NONE', #48284, 8.999999999999998224, 1.047197551196595855 ) ;
#45961=DIRECTION ( 'NONE',  ( -0.000000000000000000, -0.000000000000000000, 1.000000000000000000 ) ) ;
#46160=ADVANCED_FACE ( 'NONE', ( #20663, #55391 ), #2949, .F. ) ;
#46230=DIRECTION ( 'NONE',  ( -0.8191520442889906883, 0.000000000000000000, -0.5735764363510477137 ) ) ;
#46307=CARTESIAN_POINT ( 'NONE',  ( 9.000000000000001776, -5.196152422706648899, -0.8038475772933779684 ) ) ;
#46528=DIRECTION ( 'NONE',  ( 0.000000000000000000, -0.000000000000000000, 1.000000000000000000 ) ) ;
#46533=VECTOR ( 'NONE', #53787, 1000.000000000000000 ) ;
#46562=CARTESIAN_POINT ( 'NONE',  ( 0.000000000000000000, 0.000000000000000000, -0.6932054628276118624 ) ) ;
#46611=VECTOR ( 'NONE', #46230, 1000.000000000000114 ) ;
#46651=DIRECTION ( 'NONE',  ( 1.000000000000000000, 0.000000000000000000, 0.000000000000000000 ) ) ;
#46663=ORIENTED_EDGE ( 'NONE', *, *, #8892, .F. ) ;
#46669=CIRCLE ( 'NONE', #17735, 6.000000000000000000 ) ;
#46802=DIRECTION ( 'NONE',  ( 0.000000000000000000, 0.000000000000000000, -1.000000000000000000 ) ) ;
#46845=DIRECTION ( 'NONE',  ( -0.8660254037844380415, -0.5000000000000011102, 0.000000000000000000 ) ) ;
#47034=VERTEX_POINT ( 'NONE', #6258 ) ;
#47045=DIRECTION ( 'NONE',  ( 0.8660254037844380415, -0.5000000000000013323, 0.000000000000000000 ) ) ;
#47066=AXIS2_PLACEMENT_3D ( 'NONE', #13460, #31200, #59511 ) ;
#47117=ORIENTED_EDGE ( 'NONE', *, *, #30702, .T. ) ;
#47197=ADVANCED_FACE ( 'NONE', ( #42609 ), #65994, .F. ) ;
#47230=ORIENTED_EDGE ( 'NONE', *, *, #29495, .T. ) ;
#47354=CARTESIAN_POINT ( 'NONE',  ( -8.999999999999998224, 0.000000000000000000, 0.000000000000000000 ) ) ;
#47573=VERTEX_POINT ( 'NONE', #73634 ) ;
#47575=CARTESIAN_POINT ( 'NONE',  ( 1.334622868157815783E-15, 10.39230484541327293, -10.80000000000000071 ) ) ;
#47715=CARTESIAN_POINT ( 'NONE',  ( -9.000000000000000000, -1.750439824713162729, -0.07547478993377626511 ) ) ;
#47730=EDGE_LOOP ( 'NONE', ( #49739, #65045, #37540 ) ) ;
#47762=AXIS2_PLACEMENT_3D ( 'NONE', #46562, #11866, #5104 ) ;
#47964=ORIENTED_EDGE ( 'NONE', *, *, #38622, .F. ) ;
#48105=LINE ( 'NONE', #59449, #7974 ) ;
#48116=AXIS2_PLACEMENT_3D ( 'NONE', #59626, #24543, #53233 ) ;
#48191=ORIENTED_EDGE ( 'NONE', *, *, #23779, .F. ) ;
#48278=ORIENTED_EDGE ( 'NONE', *, *, #29495, .F. ) ;
#48284=AXIS2_PLACEMENT_3D ( 'NONE', #40606, #69650, #63608 ) ;
#48298=CARTESIAN_POINT ( 'NONE',  ( -5.099999999999999645, 6.245698675651499853E-16, -0.6301867843887376530 ) ) ;
#48337=CONICAL_SURFACE ( 'NONE', #54395, 8.999999999999998224, 1.047197551196595855 ) ;
#48460=VECTOR ( 'NONE', #40212, 1000.000000000000000 ) ;
#48606=DIRECTION ( 'NONE',  ( -1.000000000000000000, 0.000000000000000000, 0.000000000000000000 ) ) ;
#48661=ORIENTED_EDGE ( 'NONE', *, *, #38040, .T. ) ;
#48760=CARTESIAN_POINT ( 'NONE',  ( 9.000000000000000000, 4.355963544827403666, -0.5613059398865194449 ) ) ;
#48808=EDGE_CURVE ( 'NONE', #70885, #13802, #20307, .T. ) ;
#48818=ADVANCED_FACE ( 'NONE', ( #29569 ), #19254, .T. ) ;
#48850=DIRECTION ( 'NONE',  ( 1.000000000000000000, 0.000000000000000000, 0.000000000000000000 ) ) ;
#49067=AXIS2_PLACEMENT_3D ( 'NONE', #42691, #26838, #9504 ) ;
#49092=EDGE_CURVE ( 'NONE', #59754, #25774, #50165, .T. ) ;
#49335=DIRECTION ( 'NONE',  ( 0.000000000000000000, 0.000000000000000000, -1.000000000000000000 ) ) ;
#49364=ORIENTED_EDGE ( 'NONE', *, *, #2154, .F. ) ;
#49411=DIRECTION ( 'NONE',  ( 0.000000000000000000, 0.000000000000000000, -1.000000000000000000 ) ) ;
#49538=AXIS2_PLACEMENT_3D ( 'NONE', #41735, #52322, #46651 ) ;
#49548=ADVANCED_FACE ( 'NONE', ( #13128 ), #19906, .F. ) ;
#49683=DIRECTION ( 'NONE',  ( -1.000000000000000000, 0.000000000000000000, 0.000000000000000000 ) ) ;
#49739=ORIENTED_EDGE ( 'NONE', *, *, #68754, .F. ) ;
#49848=DIRECTION ( 'NONE',  ( 0.000000000000000000, 0.000000000000000000, -1.000000000000000000 ) ) ;
#49895=B_SPLINE_CURVE_WITH_KNOTS ( 'NONE', 3,
 ( #63741, #58837, #29421, #7517, #7148, #70157, #35822, #12790 ),
 .UNSPECIFIED., .F., .F.,
 ( 4, 2, 2, 4 ),
 ( 0.005257893453559909711, 0.006567392922673239916, 0.007876892391786568387, 0.01049589133001322880 ),
 .UNSPECIFIED. ) ;
#49937=ORIENTED_EDGE ( 'NONE', *, *, #21654, .F. ) ;
#49941=CARTESIAN_POINT ( 'NONE',  ( 0.000000000000000000, 20.39230484541327471, -10.20000000000000284 ) ) ;
#49992=ORIENTED_EDGE ( 'NONE', *, *, #51405, .F. ) ;
#50035=CARTESIAN_POINT ( 'NONE',  ( -4.118099735505520442, 8.014718854569423456, 4.446287698374634477E-15 ) ) ;
#50049=FACE_BOUND ( 'NONE', #41802, .T. ) ;
#50068=CARTESIAN_POINT ( 'NONE',  ( 5.009999999999998899, 0.000000000000000000, -0.6932054628276118624 ) ) ;
#50165=LINE ( 'NONE', #39596, #12305 ) ;
#50169=DIRECTION ( 'NONE',  ( 0.000000000000000000, 0.000000000000000000, 1.000000000000000000 ) ) ;
#50250=DIRECTION ( 'NONE',  ( -1.000000000000000000, 0.000000000000000000, 0.000000000000000000 ) ) ;
#50322=VERTEX_POINT ( 'NONE', #38683 ) ;
#50450=DIRECTION ( 'NONE',  ( 0.000000000000000000, 0.000000000000000000, -1.000000000000000000 ) ) ;
#50510=DIRECTION ( 'NONE',  ( 1.000000000000000000, 0.000000000000000000, 0.000000000000000000 ) ) ;
#50605=VECTOR ( 'NONE', #60145, 1000.000000000000000 ) ;
#50652=AXIS2_PLACEMENT_3D ( 'NONE', #54331, #25994, #58886 ) ;
#50673=ADVANCED_FACE ( 'NONE', ( #32941 ), #37674, .T. ) ;
#50698=CIRCLE ( 'NONE', #25376, 9.000000000000001776 ) ;
#50858=VECTOR ( 'NONE', #24368, 1000.000000000000000 ) ;
#50931=ORIENTED_EDGE ( 'NONE', *, *, #48808, .T. ) ;
#50998=AXIS2_PLACEMENT_3D ( 'NONE', #13400, #8497, #48850 ) ;
#51110=FACE_OUTER_BOUND ( 'NONE', #30067, .T. ) ;
#51237=ORIENTED_EDGE ( 'NONE', *, *, #21654, .T. ) ;
#51405=EDGE_CURVE ( 'NONE', #41903, #72372, #73854, .T. ) ;
#51627=AXIS2_PLACEMENT_3D ( 'NONE', #52025, #36156, #23345 ) ;
#51848=AXIS2_PLACEMENT_3D ( 'NONE', #59233, #41500, #7176 ) ;
#51903=LINE ( 'NONE', #34570, #43986 ) ;
#51938=CARTESIAN_POINT ( 'NONE',  ( -4.076600168545496672E-14, -10.39230484541327471, -0.8038475772933779684 ) ) ;
#52025=CARTESIAN_POINT ( 'NONE',  ( 0.000000000000000000, 0.000000000000000000, -10.20000000000000462 ) ) ;
#52094=AXIS2_PLACEMENT_3D ( 'NONE', #30553, #42600, #30914 ) ;
#52263=VECTOR ( 'NONE', #20539, 1000.000000000000000 ) ;
#52322=DIRECTION ( 'NONE',  ( -0.000000000000000000, -0.000000000000000000, 1.000000000000000000 ) ) ;
#52406=VECTOR ( 'NONE', #47045, 999.9999999999997726 ) ;
#52802=ORIENTED_EDGE ( 'NONE', *, *, #61267, .T. ) ;
#52887=DIRECTION ( 'NONE',  ( 0.8660254037844380415, -0.5000000000000013323, 0.000000000000000000 ) ) ;
#52979=APPLICATION_CONTEXT ( 'automotive_design' ) ;
#53017=DIRECTION ( 'NONE',  ( 0.000000000000000000, -1.000000000000000000, 0.000000000000000000 ) ) ;
#53093=CARTESIAN_POINT ( 'NONE',  ( -9.000000000000000000, -5.196152422706644458, -10.20000000000000284 ) ) ;
#53224=DIRECTION ( 'NONE',  ( 0.8660254037844379305, -0.5000000000000012212, 0.000000000000000000 ) ) ;
#53233=DIRECTION ( 'NONE',  ( 1.000000000000000000, 0.000000000000000000, 0.000000000000000000 ) ) ;
#53257=CARTESIAN_POINT ( 'NONE',  ( -9.000000000000000000, -5.196152422706644458, -10.20000000000000284 ) ) ;
#53296=DIRECTION ( 'NONE',  ( 1.000000000000000000, 0.000000000000000000, 0.000000000000000000 ) ) ;
#53521=ORIENTED_EDGE ( 'NONE', *, *, #26447, .T. ) ;
#53543=AXIS2_PLACEMENT_3D ( 'NONE', #56433, #5128, #10773 ) ;
#53603=CARTESIAN_POINT ( 'NONE',  ( 0.000000000000000000, 0.000000000000000000, 0.000000000000000000 ) ) ;
#53787=DIRECTION ( 'NONE',  ( 0.8660254037844381525, 0.5000000000000008882, 0.000000000000000000 ) ) ;
#53854=VECTOR ( 'NONE', #4425, 1000.000000000000000 ) ;
#53939=CARTESIAN_POINT ( 'NONE',  ( 5.099999999999999645, 0.000000000000000000, -10.14441321561125520 ) ) ;
#54013=ORIENTED_EDGE ( 'NONE', *, *, #30867, .F. ) ;
#54110=CIRCLE ( 'NONE', #62519, 5.099999999999999645 ) ;
#54194=ORIENTED_EDGE ( 'NONE', *, *, #2393, .F. ) ;
#54221=PRODUCT_DEFINITION ( 'UNKNOWN', '', #42987, #41126 ) ;
#54263=ADVANCED_FACE ( 'NONE', ( #39469 ), #23597, .T. ) ;
#54295=CIRCLE ( 'NONE', #47066, 9.000000000000001776 ) ;
#54331=CARTESIAN_POINT ( 'NONE',  ( 0.000000000000000000, 0.000000000000000000, 0.000000000000000000 ) ) ;
#54395=AXIS2_PLACEMENT_3D ( 'NONE', #31215, #46802, #29832 ) ;
#54435=CARTESIAN_POINT ( 'NONE',  ( 0.000000000000000000, 0.000000000000000000, -0.6932054628276118624 ) ) ;
#54587=ADVANCED_FACE ( 'NONE', ( #71087 ), #7208, .F. ) ;
#54698=CYLINDRICAL_SURFACE ( 'NONE', #35965, 5.099999999999999645 ) ;
#54808=CARTESIAN_POINT ( 'NONE',  ( 1.474731560294312738, -9.540868182094932592, -0.3570196857253685185 ) ) ;
#54957=ORIENTED_EDGE ( 'NONE', *, *, #22410, .T. ) ;
#54995=CARTESIAN_POINT ( 'NONE',  ( 0.000000000000000000, 0.000000000000000000, 0.000000000000000000 ) ) ;
#55053=CARTESIAN_POINT ( 'NONE',  ( -1.001543065824775909E-15, -10.39230484541329247, -10.80000000000000071 ) ) ;
#55150=ORIENTED_EDGE ( 'NONE', *, *, #17599, .T. ) ;
#55186=CARTESIAN_POINT ( 'NONE',  ( 3.734486434573635272, -8.236198097127193307, -0.01899995639454811480 ) ) ;
#55243=DIRECTION ( 'NONE',  ( 0.000000000000000000, 0.000000000000000000, 1.000000000000000000 ) ) ;
#55316=ADVANCED_FACE ( 'NONE', ( #30946 ), #29480, .T. ) ;
#55388=LINE ( 'NONE', #65189, #56121 ) ;
#55391=FACE_OUTER_BOUND ( 'NONE', #34254, .T. ) ;
#55402=EDGE_CURVE ( 'NONE', #13802, #63081, #72243, .T. ) ;
#55651=DIRECTION ( 'NONE',  ( 0.000000000000000000, 0.000000000000000000, -1.000000000000000000 ) ) ;
#55900=EDGE_CURVE ( 'NONE', #327, #8398, #866, .T. ) ;
#55948=CARTESIAN_POINT ( 'NONE',  ( 0.000000000000000000, 0.000000000000000000, 0.000000000000000000 ) ) ;
#55989=FACE_OUTER_BOUND ( 'NONE', #73429, .T. ) ;
#56121=VECTOR ( 'NONE', #26695, 1000.000000000000000 ) ;
#56134=DIRECTION ( 'NONE',  ( -1.000000000000000000, 0.000000000000000000, 0.000000000000000000 ) ) ;
#56198=CYLINDRICAL_SURFACE ( 'NONE', #65380, 6.000000000000000000 ) ;
#56231=VERTEX_POINT ( 'NONE', #68025 ) ;
#56433=CARTESIAN_POINT ( 'NONE',  ( 0.000000000000000000, 0.000000000000000000, -10.80000000000000071 ) ) ;
#56442=ORIENTED_EDGE ( 'NONE', *, *, #36684, .T. ) ;
#56536=EDGE_CURVE ( 'NONE', #63061, #62856, #15968, .T. ) ;
#56942=FACE_OUTER_BOUND ( 'NONE', #63916, .T. ) ;
#56978=FACE_OUTER_BOUND ( 'NONE', #32283, .T. ) ;
#57011=ADVANCED_FACE ( 'NONE', ( #14383 ), #10860, .T. ) ;
#57253=CARTESIAN_POINT ( 'NONE',  ( -8.999999999999998224, 0.000000000000000000, 0.000000000000000000 ) ) ;
#57354=AXIS2_PLACEMENT_3D ( 'NONE', #63097, #11422, #34459 ) ;
#57544=ADVANCED_FACE ( 'NONE', ( #64878 ), #13179, .T. ) ;
#57624=ORIENTED_EDGE ( 'NONE', *, *, #44825, .F. ) ;
#57632=DIRECTION ( 'NONE',  ( -0.000000000000000000, -0.000000000000000000, 1.000000000000000000 ) ) ;
#57937=VERTEX_POINT ( 'NONE', #40375 ) ;
#57958=DIRECTION ( 'NONE',  ( 0.5000000000000014433, 0.8660254037844379305, -0.000000000000000000 ) ) ;
#58029=CARTESIAN_POINT ( 'NONE',  ( 8.999999999999998224, 0.000000000000000000, 0.000000000000000000 ) ) ;
#58263=CARTESIAN_POINT ( 'NONE',  ( 0.000000000000000000, 0.000000000000000000, -10.20000000000000462 ) ) ;
#58330=ORIENTED_EDGE ( 'NONE', *, *, #42112, .T. ) ;
#58331=CARTESIAN_POINT ( 'NONE',  ( -7.522341449313134198, 6.049278984716041307, -0.3563104543936375102 ) ) ;
#58333=CARTESIAN_POINT ( 'NONE',  ( -9.000000000000001776, -4.351040328464083728, -0.5598847297401622347 ) ) ;
#58386=ORIENTED_EDGE ( 'NONE', *, *, #11012, .F. ) ;
#58520=PLANE ( 'NONE',  #40809 ) ;
#58600=DIRECTION ( 'NONE',  ( 0.000000000000000000, -0.000000000000000000, 1.000000000000000000 ) ) ;
#58619=ORIENTED_EDGE ( 'NONE', *, *, #64089, .F. ) ;
#58687=CARTESIAN_POINT ( 'NONE',  ( 0.000000000000000000, 0.000000000000000000, -10.77459999999999951 ) ) ;
#58781=ORIENTED_EDGE ( 'NONE', *, *, #29122, .T. ) ;
#58798=EDGE_LOOP ( 'NONE', ( #39404, #10960 ) ) ;
#58805=CARTESIAN_POINT ( 'NONE',  ( 6.000000000000000000, 7.347880794884119736E-16, -10.77459999999999951 ) ) ;
#58837=CARTESIAN_POINT ( 'NONE',  ( 4.881900264494500874, 7.573738413550456627, 4.181378144120852046E-15 ) ) ;
#58885=EDGE_CURVE ( 'NONE', #61426, #15999, #50698, .T. ) ;
#58886=DIRECTION ( 'NONE',  ( -1.000000000000000000, 1.776356839400250465E-15, 0.000000000000000000 ) ) ;
#58971=CARTESIAN_POINT ( 'NONE',  ( 0.000000000000000000, 0.000000000000000000, -10.80000000000000071 ) ) ;
#58990=CARTESIAN_POINT ( 'NONE',  ( 0.000000000000000000, 0.000000000000000000, 0.000000000000000000 ) ) ;
#59069=VECTOR ( 'NONE', #55243, 1000.000000000000000 ) ;
#59079=CARTESIAN_POINT ( 'NONE',  ( -4.500000000000012434, 7.794228634059945371, -10.20000000000000462 ) ) ;
#59233=CARTESIAN_POINT ( 'NONE',  ( 0.000000000000000000, 20.39230484541327471, -10.20000000000000284 ) ) ;
#59281=ORIENTED_EDGE ( 'NONE', *, *, #70153, .F. ) ;
#59353=CARTESIAN_POINT ( 'NONE',  ( 4.500000000000006217, -7.794228634059941818, 0.000000000000000000 ) ) ;
#59396=EDGE_CURVE ( 'NONE', #15999, #39667, #37132, .T. ) ;
#59440=CARTESIAN_POINT ( 'NONE',  ( 8.999999999999998224, 0.000000000000000000, 0.000000000000000000 ) ) ;
#59449=CARTESIAN_POINT ( 'NONE',  ( 6.000000000000000000, 7.347880794884119736E-16, -10.77459999999999951 ) ) ;
#59452=CARTESIAN_POINT ( 'NONE',  ( -1.001543065824775909E-15, -10.39230484541329247, -10.80000000000000071 ) ) ;
#59511=DIRECTION ( 'NONE',  ( -1.000000000000000000, 0.000000000000000000, 0.000000000000000000 ) ) ;
#59563=ADVANCED_FACE ( 'NONE', ( #67484 ), #72772, .T. ) ;
#59564=ADVANCED_FACE ( 'NONE', ( #9394 ), #32414, .T. ) ;
#59580=ORIENTED_EDGE ( 'NONE', *, *, #10673, .T. ) ;
#59626=CARTESIAN_POINT ( 'NONE',  ( 0.000000000000000000, 0.000000000000000000, 0.000000000000000000 ) ) ;
#59749=ADVANCED_FACE ( 'NONE', ( #8664 ), #54698, .F. ) ;
#59754=VERTEX_POINT ( 'NONE', #44120 ) ;
#59761=CIRCLE ( 'NONE', #69407, 5.099999999999999645 ) ;
#59776=CONICAL_SURFACE ( 'NONE', #45350, 8.999999999999998224, 1.047197551196595855 ) ;
#59810=ORIENTED_EDGE ( 'NONE', *, *, #56536, .F. ) ;
#59896=DIRECTION ( 'NONE',  ( -1.000000000000000000, 0.000000000000000000, 0.000000000000000000 ) ) ;
#59991=CARTESIAN_POINT ( 'NONE',  ( 0.7361406979141439377, 9.967293815311101923, -0.5584673446549246467 ) ) ;
#59993=VERTEX_POINT ( 'NONE', #53939 ) ;
#60145=DIRECTION ( 'NONE',  ( 0.000000000000000000, 0.000000000000000000, 1.000000000000000000 ) ) ;
#60283=DIRECTION ( 'NONE',  ( -1.000000000000000000, 0.000000000000000000, 0.000000000000000000 ) ) ;
#60290=CIRCLE ( 'NONE', #50652, 8.999999999999998224 ) ;
#60298=DIRECTION ( 'NONE',  ( 0.000000000000000000, -0.000000000000000000, 1.000000000000000000 ) ) ;
#60325=PLANE ( 'NONE',  #52094 ) ;
#60468=ORIENTED_EDGE ( 'NONE', *, *, #51405, .T. ) ;
#60510=PLANE ( 'NONE',  #66508 ) ;
#60689=ORIENTED_EDGE ( 'NONE', *, *, #6206, .F. ) ;
#60699=DIRECTION ( 'NONE',  ( -0.000000000000000000, -0.000000000000000000, 1.000000000000000000 ) ) ;
#60882=ADVANCED_FACE ( 'NONE', ( #64172 ), #58520, .T. ) ;
#60930=ORIENTED_EDGE ( 'NONE', *, *, #44016, .F. ) ;
#61020=DIRECTION ( 'NONE',  ( 0.000000000000000000, 0.000000000000000000, -1.000000000000000000 ) ) ;
#61112=CARTESIAN_POINT ( 'NONE',  ( -7.525268439705684820, -6.047589086025006999, -0.3570196857253580824 ) ) ;
#61258=CARTESIAN_POINT ( 'NONE',  ( -5.099999999999999645, 6.245698675651499853E-16, -10.80000000000000071 ) ) ;
#61267=EDGE_CURVE ( 'NONE', #72372, #59754, #43218, .T. ) ;
#61297=CARTESIAN_POINT ( 'NONE',  ( 0.000000000000000000, 0.000000000000000000, -0.6301867843887376530 ) ) ;
#61318=ORIENTED_EDGE ( 'NONE', *, *, #2080, .F. ) ;
#61359=CARTESIAN_POINT ( 'NONE',  ( -2.598723904613012614, 8.891930899535427812, -0.1469846612282519061 ) ) ;
#61426=VERTEX_POINT ( 'NONE', #14607 ) ;
#61563=DIRECTION ( 'NONE',  ( 1.000000000000000000, 0.000000000000000000, 0.000000000000000000 ) ) ;
#61580=CARTESIAN_POINT ( 'NONE',  ( 0.000000000000000000, 0.000000000000000000, -10.14441321561125520 ) ) ;
#61744=AXIS2_PLACEMENT_3D ( 'NONE', #55948, #44614, #72149 ) ;
#61747=VECTOR ( 'NONE', #64913, 1000.000000000000000 ) ;
#61811=ORIENTED_EDGE ( 'NONE', *, *, #35808, .T. ) ;
#61864=LINE ( 'NONE', #10928, #29604 ) ;
#61956=VERTEX_POINT ( 'NONE', #51938 ) ;
#62017=CARTESIAN_POINT ( 'NONE',  ( 6.000000000000000000, 0.000000000000000000, 0.000000000000000000 ) ) ;
#62039=ORIENTED_EDGE ( 'NONE', *, *, #69688, .F. ) ;
#62080=ORIENTED_EDGE ( 'NONE', *, *, #66727, .F. ) ;
#62100=CARTESIAN_POINT ( 'NONE',  ( -3.734486434573632163, 8.236198097127171991, -0.01899995639453642277 ) ) ;
#62121=EDGE_CURVE ( 'NONE', #44162, #71873, #8819, .T. ) ;
#62299=B_SPLINE_CURVE_WITH_KNOTS ( 'NONE', 3,
 ( #8404, #3879, #31417, #43098, #48760, #73279 ),
 .UNSPECIFIED., .F., .F.,
 ( 4, 2, 4 ),
 ( 0.01452727543195641083, 0.01715716534226974926, 0.01978705525258308423 ),
 .UNSPECIFIED. ) ;
#62440=AXIS2_PLACEMENT_3D ( 'NONE', #55053, #2986, #66354 ) ;
#62519=AXIS2_PLACEMENT_3D ( 'NONE', #19182, #8609, #60283 ) ;
#62615=PLANE ( 'NONE',  #12861 ) ;
#62845=CARTESIAN_POINT ( 'NONE',  ( 4.500000000000010658, 7.794228634059937377, 0.000000000000000000 ) ) ;
#62856=VERTEX_POINT ( 'NONE', #48298 ) ;
#62894=DIRECTION ( 'NONE',  ( 1.000000000000000000, 0.000000000000000000, 0.000000000000000000 ) ) ;
#63061=VERTEX_POINT ( 'NONE', #31565 ) ;
#63081=VERTEX_POINT ( 'NONE', #25880 ) ;
#63097=CARTESIAN_POINT ( 'NONE',  ( 0.000000000000000000, 0.000000000000000000, 0.000000000000000000 ) ) ;
#63129=VECTOR ( 'NONE', #13050, 1000.000000000000000 ) ;
#63162=DIRECTION ( 'NONE',  ( 0.000000000000000000, 0.000000000000000000, 1.000000000000000000 ) ) ;
#63608=DIRECTION ( 'NONE',  ( -1.000000000000000000, 0.000000000000000000, 0.000000000000000000 ) ) ;
#63739=AXIS2_PLACEMENT_3D ( 'NONE', #34946, #57958, #39834 ) ;
#63741=CARTESIAN_POINT ( 'NONE',  ( 4.500000000000010658, 7.794228634059937377, 0.000000000000000000 ) ) ;
#63755=ORIENTED_EDGE ( 'NONE', *, *, #668, .T. ) ;
#63916=EDGE_LOOP ( 'NONE', ( #20875, #25565, #51237, #5376 ) ) ;
#64089=EDGE_CURVE ( 'NONE', #64865, #41819, #45074, .T. ) ;
#64172=FACE_OUTER_BOUND ( 'NONE', #25836, .T. ) ;
#64199=UNCERTAINTY_MEASURE_WITH_UNIT (LENGTH_MEASURE( 1.000000000000000082E-05 ), #28451, 'distance_accuracy_value', 'NONE');
#64540=CARTESIAN_POINT ( 'NONE',  ( -9.000000000000000000, -5.196152422706644458, -10.80000000000000071 ) ) ;
#64706=DIRECTION ( 'NONE',  ( -1.000000000000000000, 0.000000000000000000, 0.000000000000000000 ) ) ;
#64752=CARTESIAN_POINT ( 'NONE',  ( -9.000000000000001776, 1.102182119232617911E-15, 0.000000000000000000 ) ) ;
#64865=VERTEX_POINT ( 'NONE', #57253 ) ;
#64878=FACE_OUTER_BOUND ( 'NONE', #36869, .T. ) ;
#64913=DIRECTION ( 'NONE',  ( -0.000000000000000000, -0.000000000000000000, 1.000000000000000000 ) ) ;
#65045=ORIENTED_EDGE ( 'NONE', *, *, #2154, .T. ) ;
#65189=CARTESIAN_POINT ( 'NONE',  ( 9.000000000000000000, 5.196152422706622254, -10.80000000000000071 ) ) ;
#65197=( GEOMETRIC_REPRESENTATION_CONTEXT ( 3 ) GLOBAL_UNCERTAINTY_ASSIGNED_CONTEXT ( ( #64199 ) ) GLOBAL_UNIT_ASSIGNED_CONTEXT ( ( #28451, #5082, #74101 ) ) REPRESENTATION_CONTEXT ( 'NONE', 'WORKASPACE' ) );
#65291=ORIENTED_EDGE ( 'NONE', *, *, #8536, .T. ) ;
#65380=AXIS2_PLACEMENT_3D ( 'NONE', #4511, #33202, #22586 ) ;
#65408=CARTESIAN_POINT ( 'NONE',  ( 5.266666970006220083, -7.351593252548084045, -6.728829732988161894E-15 ) ) ;
#65498=EDGE_LOOP ( 'NONE', ( #59810, #54013, #29093, #59281 ) ) ;
#65518=PRODUCT_DEFINITION_SHAPE ( 'NONE', 'NONE',  #54221 ) ;
#65581=VERTEX_POINT ( 'NONE', #6420 ) ;
#65648=CARTESIAN_POINT ( 'NONE',  ( 1.477658550686875349, 9.539178283403852987, -0.3563104543936415625 ) ) ;
#65703=PLANE ( 'NONE',  #49067 ) ;
#65769=CARTESIAN_POINT ( 'NONE',  ( 0.000000000000000000, 0.000000000000000000, 0.000000000000000000 ) ) ;
#65932=CARTESIAN_POINT ( 'NONE',  ( 0.000000000000000000, 0.000000000000000000, -10.80000000000000071 ) ) ;
#65994=PLANE ( 'NONE',  #9833 ) ;
#66001=ORIENTED_EDGE ( 'NONE', *, *, #2393, .T. ) ;
#66020=CARTESIAN_POINT ( 'NONE',  ( -4.500000000000010658, -7.794228634059939154, 0.000000000000000000 ) ) ;
#66150=EDGE_CURVE ( 'NONE', #47034, #41903, #18388, .T. ) ;
#66354=DIRECTION ( 'NONE',  ( 0.8660254037844381525, 0.5000000000000008882, 0.000000000000000000 ) ) ;
#66482=ORIENTED_EDGE ( 'NONE', *, *, #22410, .F. ) ;
#66508=AXIS2_PLACEMENT_3D ( 'NONE', #49941, #32609, #37133 ) ;
#66628=ORIENTED_EDGE ( 'NONE', *, *, #14645, .T. ) ;
#66727=EDGE_CURVE ( 'NONE', #63081, #70885, #41562, .T. ) ;
#66836=FACE_OUTER_BOUND ( 'NONE', #31272, .T. ) ;
#66888=EDGE_CURVE ( 'NONE', #12586, #15999, #51903, .T. ) ;
#66925=CARTESIAN_POINT ( 'NONE',  ( 1.334622868157815783E-15, 10.39230484541327293, -10.80000000000000071 ) ) ;
#67008=EDGE_LOOP ( 'NONE', ( #18022, #15836, #12684, #70460 ) ) ;
#67110=DIRECTION ( 'NONE',  ( -1.000000000000000000, 0.000000000000000000, -0.000000000000000000 ) ) ;
#67226=FACE_OUTER_BOUND ( 'NONE', #8638, .T. ) ;
#67446=CARTESIAN_POINT ( 'NONE',  ( 6.938893903907228378E-15, 10.39230484541326938, 0.000000000000000000 ) ) ;
#67484=FACE_OUTER_BOUND ( 'NONE', #40156, .T. ) ;
#67685=DIRECTION ( 'NONE',  ( 1.000000000000000000, 0.000000000000000000, 0.000000000000000000 ) ) ;
#67729=AXIS2_PLACEMENT_3D ( 'NONE', #42636, #49411, #8308 ) ;
#67815=CARTESIAN_POINT ( 'NONE',  ( 0.000000000000000000, 0.000000000000000000, 0.000000000000000000 ) ) ;
#67965=CYLINDRICAL_SURFACE ( 'NONE', #74418, 9.000000000000001776 ) ;
#68025=CARTESIAN_POINT ( 'NONE',  ( -6.000000000000000000, 7.347880794884119736E-16, -10.80000000000000071 ) ) ;
#68304=ORIENTED_EDGE ( 'NONE', *, *, #26977, .T. ) ;
#68344=CARTESIAN_POINT ( 'NONE',  ( -9.000000000000000000, 1.769118300197570104, -0.07756262466202451522 ) ) ;
#68348=EDGE_CURVE ( 'NONE', #327, #4091, #13689, .T. ) ;
#68389=DIRECTION ( 'NONE',  ( 0.000000000000000000, -1.000000000000000000, 0.000000000000000000 ) ) ;
#68503=CARTESIAN_POINT ( 'NONE',  ( -2.975619346028166579, 8.674330214978043685, -0.09252763182292181310 ) ) ;
#68576=CARTESIAN_POINT ( 'NONE',  ( 9.000000000000000000, -0.8780643052077397037, -1.070649645329435629E-15 ) ) ;
#68581=EDGE_CURVE ( 'NONE', #59754, #61426, #39253, .T. ) ;
#68711=CARTESIAN_POINT ( 'NONE',  ( -9.000000000000000000, 4.355963544827382350, -0.5613059398865143379 ) ) ;
#68754=EDGE_CURVE ( 'NONE', #39667, #47034, #17072, .T. ) ;
#68819=ORIENTED_EDGE ( 'NONE', *, *, #61267, .F. ) ;
#68903=AXIS2_PLACEMENT_3D ( 'NONE', #65932, #36902, #41815 ) ;
#69041=CARTESIAN_POINT ( 'NONE',  ( 6.000000000000000000, 0.000000000000000000, -10.80000000000000071 ) ) ;
#69132=ORIENTED_EDGE ( 'NONE', *, *, #35656, .T. ) ;
#69140=ORIENTED_EDGE ( 'NONE', *, *, #73700, .T. ) ;
#69172=DIRECTION ( 'NONE',  ( 0.000000000000000000, 0.000000000000000000, -1.000000000000000000 ) ) ;
#69396=VERTEX_POINT ( 'NONE', #18120 ) ;
#69407=AXIS2_PLACEMENT_3D ( 'NONE', #20520, #9218, #67685 ) ;
#69650=DIRECTION ( 'NONE',  ( 0.000000000000000000, 0.000000000000000000, -1.000000000000000000 ) ) ;
#69687=AXIS2_PLACEMENT_3D ( 'NONE', #27478, #60699, #15405 ) ;
#69688=EDGE_CURVE ( 'NONE', #69396, #39667, #19954, .T. ) ;
#69794=ORIENTED_EDGE ( 'NONE', *, *, #30867, .T. ) ;
#70011=CARTESIAN_POINT ( 'NONE',  ( -6.023803224821316249, 6.914460432017338398, -0.07661102881317759239 ) ) ;
#70013=CARTESIAN_POINT ( 'NONE',  ( -9.000000000000000000, -3.485479754112952744, -0.3552645118408633285 ) ) ;
#70077=EDGE_LOOP ( 'NONE', ( #61318, #6241, #2233 ) ) ;
#70153=EDGE_CURVE ( 'NONE', #62856, #47573, #59761, .T. ) ;
#70157=CARTESIAN_POINT ( 'NONE',  ( 7.525268439705678603, 6.047589086024989236, -0.3570196857253479794 ) ) ;
#70216=DIRECTION ( 'NONE',  ( 0.000000000000000000, -0.000000000000000000, 1.000000000000000000 ) ) ;
#70223=CARTESIAN_POINT ( 'NONE',  ( -6.000000000000000000, 7.347880794884119736E-16, -25.03750572909317285 ) ) ;
#70322=EDGE_LOOP ( 'NONE', ( #14145, #48191, #8668, #34201 ) ) ;
#70347=CARTESIAN_POINT ( 'NONE',  ( 7.522341449313136863, -6.049278984716062624, -0.3563104543936467805 ) ) ;
#70398=LINE ( 'NONE', #36803, #46533 ) ;
#70410=CYLINDRICAL_SURFACE ( 'NONE', #49538, 6.000000000000000000 ) ;
#70460=ORIENTED_EDGE ( 'NONE', *, *, #72837, .F. ) ;
#70885=VERTEX_POINT ( 'NONE', #10625 ) ;
#71087=FACE_OUTER_BOUND ( 'NONE', #74309, .T. ) ;
#71243=ORIENTED_EDGE ( 'NONE', *, *, #27269, .F. ) ;
#71248=PRODUCT_CONTEXT ( 'NONE', #33707, 'mechanical' ) ;
#71301=CARTESIAN_POINT ( 'NONE',  ( 3.733333029993803898, 8.236864015571821795, 4.143685177968037259E-15 ) ) ;
#71873=VERTEX_POINT ( 'NONE', #9336 ) ;
#72023=CARTESIAN_POINT ( 'NONE',  ( 0.000000000000000000, 0.000000000000000000, -10.80000000000000071 ) ) ;
#72104=CARTESIAN_POINT ( 'NONE',  ( 0.000000000000000000, 0.000000000000000000, 0.000000000000000000 ) ) ;
#72149=DIRECTION ( 'NONE',  ( -1.000000000000000000, 0.000000000000000000, 0.000000000000000000 ) ) ;
#72176=DIRECTION ( 'NONE',  ( -0.000000000000000000, -0.000000000000000000, 1.000000000000000000 ) ) ;
#72243=CIRCLE ( 'NONE', #16818, 8.999999999999998224 ) ;
#72372=VERTEX_POINT ( 'NONE', #36625 ) ;
#72388=DIRECTION ( 'NONE',  ( 0.000000000000000000, 0.000000000000000000, -1.000000000000000000 ) ) ;
#72443=AXIS2_PLACEMENT_3D ( 'NONE', #58971, #58600, #1265 ) ;
#72468=EDGE_LOOP ( 'NONE', ( #28227, #19112, #22070 ) ) ;
#72545=B_SPLINE_CURVE_WITH_KNOTS ( 'NONE', 3,
 ( #11007, #22679, #68344, #16640, #68711, #34409 ),
 .UNSPECIFIED., .F., .F.,
 ( 4, 2, 4 ),
 ( 0.01452727543195641083, 0.01715716534226973539, 0.01978705525258305647 ),
 .UNSPECIFIED. ) ;
#72731=CARTESIAN_POINT ( 'NONE',  ( 9.000000000000000000, 5.196152422706622254, -10.20000000000000284 ) ) ;
#72754=CARTESIAN_POINT ( 'NONE',  ( 0.000000000000000000, 0.000000000000000000, 0.000000000000000000 ) ) ;
#72772=PLANE ( 'NONE',  #62440 ) ;
#72775=CIRCLE ( 'NONE', #16146, 8.999999999999998224 ) ;
#72837=EDGE_CURVE ( 'NONE', #59993, #47573, #61864, .T. ) ;
#72844=ORIENTED_EDGE ( 'NONE', *, *, #64089, .T. ) ;
#72949=AXIS2_PLACEMENT_3D ( 'NONE', #67815, #50450, #56134 ) ;
#73065=FACE_OUTER_BOUND ( 'NONE', #58798, .T. ) ;
#73089=CARTESIAN_POINT ( 'NONE',  ( 0.000000000000000000, 0.000000000000000000, -10.77459999999999951 ) ) ;
#73161=EDGE_CURVE ( 'NONE', #30116, #31722, #55388, .T. ) ;
#73279=CARTESIAN_POINT ( 'NONE',  ( 9.000000000000000000, 5.196152422706648899, -0.8038475772933779684 ) ) ;
#73284=ADVANCED_FACE ( 'NONE', ( #38780 ), #711, .T. ) ;
#73368=CARTESIAN_POINT ( 'NONE',  ( 0.000000000000000000, 0.000000000000000000, 0.000000000000000000 ) ) ;
#73429=EDGE_LOOP ( 'NONE', ( #16014, #13218, #52802 ) ) ;
#73441=ORIENTED_EDGE ( 'NONE', *, *, #20370, .T. ) ;
#73458=DIRECTION ( 'NONE',  ( -1.000000000000000000, 0.000000000000000000, 0.000000000000000000 ) ) ;
#73505=CARTESIAN_POINT ( 'NONE',  ( 0.000000000000000000, 20.39230484541327471, -10.20000000000000284 ) ) ;
#73634=CARTESIAN_POINT ( 'NONE',  ( 5.099999999999999645, 0.000000000000000000, -0.6301867843887376530 ) ) ;
#73663=MECHANICAL_DESIGN_GEOMETRIC_PRESENTATION_REPRESENTATION('',(#31491),#65197);
#73700=EDGE_CURVE ( 'NONE', #19857, #6721, #33236, .T. ) ;
#73854=CIRCLE ( 'NONE', #13615, 9.000000000000001776 ) ;
#73859=ORIENTED_EDGE ( 'NONE', *, *, #11012, .T. ) ;
#74101=( NAMED_UNIT ( * ) SI_UNIT ( $, .STERADIAN. ) SOLID_ANGLE_UNIT ( ) );
#74204=VECTOR ( 'NONE', #68389, 1000.000000000000000 ) ;
#74309=EDGE_LOOP ( 'NONE', ( #20540, #69794, #54957, #686 ) ) ;
#74312=CARTESIAN_POINT ( 'NONE',  ( -2.976196775178717946, -8.673996836102558561, -0.07661102881318875013 ) ) ;
#74418=AXIS2_PLACEMENT_3D ( 'NONE', #17013, #22295, #61563 ) ;
#74455=CARTESIAN_POINT ( 'NONE',  ( -5.009999999999998899, 6.135480463728238062E-16, -0.6932054628276118624 ) ) ;
#74700=COLOUR_RGB('Black',0.12,0.14,0.17);
#74701=FILL_AREA_STYLE_COLOUR('',#74700);
#74702=FILL_AREA_STYLE('',(#74701));
#74703=SURFACE_STYLE_FILL_AREA(#74702);
#74704=SURFACE_SIDE_STYLE('',(#74703));
#74705=SURFACE_STYLE_USAGE(.BOTH.,#74704);
#74706=PRESENTATION_STYLE_ASSIGNMENT((#74705));
ENDSEC;
END-ISO-10303-21;
